ISO-10303-21;
HEADER;
FILE_DESCRIPTION (('STEP AP214'),
    '1' );
FILE_NAME ('right arm.step',
    '2026-10-28T16:30:29',
    ( '' ),
    ( '' ),
    'SwSTEP 2.0',
    'SolidWorks 2025',
    '' );
FILE_SCHEMA (( 'AUTOMOTIVE_DESIGN' ));
ENDSEC;

DATA;
#8=ORIENTED_EDGE ( 'NONE', *, *, #2095, .F. ) ;
#30=AXIS2_PLACEMENT_3D ( 'NONE', #3464, #4542, #1564 ) ;
#34=DIRECTION ( 'NONE',  ( 1.000000000000000000, 2.465190328815661892E-32, -9.244463733058732095E-33 ) ) ;
#61=EDGE_LOOP ( 'NONE', ( #832, #7441, #3199, #4016 ) ) ;
#62=DIRECTION ( 'NONE',  ( 0.000000000000000000, 0.000000000000000000, 1.000000000000000000 ) ) ;
#69=ORIENTED_EDGE ( 'NONE', *, *, #4461, .T. ) ;
#70=DIRECTION ( 'NONE',  ( -1.368455531567204171E-48, -0.1736481776669304422, -0.9848077530122080203 ) ) ;
#78=EDGE_LOOP ( 'NONE', ( #6432, #8, #7430, #5841, #2401, #1388, #6356, #5368 ) ) ;
#84=CARTESIAN_POINT ( 'NONE',  ( -53.48785751550376233, -228.1620966263577657, 74.64757051591519144 ) ) ;
#86=CARTESIAN_POINT ( 'NONE',  ( -30.49999999999998579, -218.0630240738404950, 95.20959099461346398 ) ) ;
#96=DIRECTION ( 'NONE',  ( 3.379803290564627601E-16, -1.193489751472043281E-15, 1.000000000000000000 ) ) ;
#100=EDGE_LOOP ( 'NONE', ( #3777, #3352, #1778, #3381, #5909, #4070 ) ) ;
#101=AXIS2_PLACEMENT_3D ( 'NONE', #3506, #6921, #4007 ) ;
#104=DIRECTION ( 'NONE',  ( -2.465190328815661892E-32, -1.000000000000000000, -1.193489751472043281E-15 ) ) ;
#106=APPLICATION_CONTEXT ( 'automotive_design' ) ;
#112=PLANE ( 'NONE',  #4971 ) ;
#121=CARTESIAN_POINT ( 'NONE',  ( -70.24881022415625864, -213.6786602093778527, 88.60457046541068848 ) ) ;
#123=CARTESIAN_POINT ( 'NONE',  ( -57.55570709107922767, -218.0630177787537605, 94.33845620223004858 ) ) ;
#127=EDGE_LOOP ( 'NONE', ( #2501, #1142, #956, #2609 ) ) ;
#143=EDGE_CURVE ( 'NONE', #589, #4118, #1720, .T. ) ;
#145=CARTESIAN_POINT ( 'NONE',  ( -64.50000000000000000, -105.5631177942458407, 67.24940929526127320 ) ) ;
#149=CARTESIAN_POINT ( 'NONE',  ( -56.14779210138475918, -223.0637666356699071, 73.66476142575187680 ) ) ;
#156=VECTOR ( 'NONE', #2539, 1000.000000000000000 ) ;
#158=CARTESIAN_POINT ( 'NONE',  ( -70.08493024494319457, -223.4607234779400642, 79.16428349862681557 ) ) ;
#160=CARTESIAN_POINT ( 'NONE',  ( -57.59964905045998762, -218.0630227653799693, 94.31979920232429038 ) ) ;
#181=EDGE_CURVE ( 'NONE', #5543, #2174, #5180, .T. ) ;
#184=CARTESIAN_POINT ( 'NONE',  ( -26.50000000000003197, -39.68629150101523351, 15.99999999999998579 ) ) ;
#185=CARTESIAN_POINT ( 'NONE',  ( -64.42620118284322928, -223.0639116415348155, 83.46765639585603935 ) ) ;
#186=CARTESIAN_POINT ( 'NONE',  ( -21.50000000000000000, -215.0630240738404950, 94.68061005248806339 ) ) ;
#192=VECTOR ( 'NONE', #6509, 1000.000000000000114 ) ;
#196=EDGE_CURVE ( 'NONE', #5318, #2388, #1106, .T. ) ;
#198=CARTESIAN_POINT ( 'NONE',  ( -53.17910001414514198, -221.3248423084432943, 72.81553374298380277 ) ) ;
#200=CARTESIAN_POINT ( 'NONE',  ( -60.96625293780100918, -218.0629435954679707, 92.08651146675032351 ) ) ;
#208=VERTEX_POINT ( 'NONE', #3488 ) ;
#224=CARTESIAN_POINT ( 'NONE',  ( -63.57431139349281324, -223.0630270109929825, 80.23469423765578767 ) ) ;
#228=VERTEX_POINT ( 'NONE', #5257 ) ;
#232=CARTESIAN_POINT ( 'NONE',  ( -53.97164445155914336, -218.0630240738405234, 95.20959099461349240 ) ) ;
#249=CARTESIAN_POINT ( 'NONE',  ( -64.50000000000000000, -99.90626354475342907, 72.90626354475362803 ) ) ;
#255=CARTESIAN_POINT ( 'NONE',  ( -26.49999999999998934, -214.0630240738404666, 94.50428307177961074 ) ) ;
#257=CARTESIAN_POINT ( 'NONE',  ( -55.78429200775497065, -223.0639285917831955, 73.57192785026977333 ) ) ;
#266=DIRECTION ( 'NONE',  ( -2.389881825834861318E-16, 0.7071067811865465735, -0.7071067811865484609 ) ) ;
#270=AXIS2_PLACEMENT_3D ( 'NONE', #1139, #3498, #377 ) ;
#282=ORIENTED_EDGE ( 'NONE', *, *, #4275, .F. ) ;
#291=LINE ( 'NONE', #789, #7056 ) ;
#293=CARTESIAN_POINT ( 'NONE',  ( -62.09225886469350542, -223.0636046126283532, 77.65152759874978017 ) ) ;
#312=VERTEX_POINT ( 'NONE', #2479 ) ;
#321=ORIENTED_EDGE ( 'NONE', *, *, #3681, .F. ) ;
#322=SHAPE_REPRESENTATION_RELATIONSHIP ( 'NONE' , 'NONE' ,  #7252, #961 ) ;
#323=CARTESIAN_POINT ( 'NONE',  ( -60.67236366837563111, -212.7665347604139185, 94.27567702561840690 ) ) ;
#325=( NAMED_UNIT ( * ) SI_UNIT ( $, .STERADIAN. ) SOLID_ANGLE_UNIT ( ) );
#331=CYLINDRICAL_SURFACE ( 'NONE', #4966, 6.000000000000000000 ) ;
#336=EDGE_CURVE ( 'NONE', #5394, #4282, #7244, .T. ) ;
#340=CARTESIAN_POINT ( 'NONE',  ( -26.50000000000003197, 0.000000000000000000, -15.99999999999998579 ) ) ;
#347=CARTESIAN_POINT ( 'NONE',  ( -21.50000000000000000, -114.3401965514817960, 42.31370849898471675 ) ) ;
#349=CARTESIAN_POINT ( 'NONE',  ( -32.50000000000002842, 6.938893903907228378E-15, 0.000000000000000000 ) ) ;
#353=CARTESIAN_POINT ( 'NONE',  ( -60.80066350777957496, -221.4565245236573787, 95.80795668296072165 ) ) ;
#363=EDGE_CURVE ( 'NONE', #7339, #580, #4329, .T. ) ;
#364=CARTESIAN_POINT ( 'NONE',  ( -58.06022122231924953, -223.0629902891046754, 95.07455849590682817 ) ) ;
#368=CARTESIAN_POINT ( 'NONE',  ( -60.60568960484322787, -218.0627689607302386, 92.42072044652158525 ) ) ;
#377=DIRECTION ( 'NONE',  ( 0.000000000000000000, 0.000000000000000000, 1.000000000000000000 ) ) ;
#382=ORIENTED_EDGE ( 'NONE', *, *, #143, .F. ) ;
#386=CARTESIAN_POINT ( 'NONE',  ( -26.50000000000003197, -99.90626354475344328, 72.90626354475362803 ) ) ;
#388=DIRECTION ( 'NONE',  ( 0.000000000000000000, 0.000000000000000000, 1.000000000000000000 ) ) ;
#389=FACE_BOUND ( 'NONE', #4788, .T. ) ;
#393=CARTESIAN_POINT ( 'NONE',  ( -53.50256896896190995, -223.7273137069649636, 96.20835808348057583 ) ) ;
#401=CARTESIAN_POINT ( 'NONE',  ( -54.18008430849435086, -223.0630240738405519, 96.09122589815579829 ) ) ;
#402=CARTESIAN_POINT ( 'NONE',  ( -32.50000000000002132, -39.68629150101521219, 24.00000000000002132 ) ) ;
#411=DIRECTION ( 'NONE',  ( 3.379803290564627601E-16, 0.000000000000000000, 1.000000000000000000 ) ) ;
#421=( BOUNDED_CURVE ( )  B_SPLINE_CURVE ( 3, ( #2509, #4253, #5516, #3784 ),
 .UNSPECIFIED., .F., .T. ) 
 B_SPLINE_CURVE_WITH_KNOTS ( ( 4, 4 ),
 ( 4.712388980384687898, 5.585053606381843672 ),
 .UNSPECIFIED. ) 
 CURVE ( )  GEOMETRIC_REPRESENTATION_ITEM ( )  RATIONAL_B_SPLINE_CURVE ( ( 1.000000000000000000, 0.9375385246911012160, 0.9375385246911012160, 1.000000000000000000 ) ) 
 REPRESENTATION_ITEM ( '' )  );
#432=CARTESIAN_POINT ( 'NONE',  ( -29.64230087749237441, 16.00000000000007105, 38.39789427971190605 ) ) ;
#439=DIRECTION ( 'NONE',  ( -2.465190328815661892E-32, -1.000000000000000000, -1.193489751472043281E-15 ) ) ;
#446=CARTESIAN_POINT ( 'NONE',  ( -61.66056754332376499, -223.0629452613760577, 92.37656864897833486 ) ) ;
#450=CARTESIAN_POINT ( 'NONE',  ( -63.60296540135762200, -218.0630256771593167, 79.14794472078611420 ) ) ;
#458=ORIENTED_EDGE ( 'NONE', *, *, #2945, .F. ) ;
#469=CARTESIAN_POINT ( 'NONE',  ( -53.29386626619290723, -219.0153713307822443, 95.37751551101598579 ) ) ;
#478=CARTESIAN_POINT ( 'NONE',  ( -61.82581114567872760, -223.0628484516971923, 92.18631465749969323 ) ) ;
#480=LINE ( 'NONE', #4569, #5650 ) ;
#481=CARTESIAN_POINT ( 'NONE',  ( -57.51269236885188008, -218.0630271768473278, 72.88129350492478409 ) ) ;
#502=VECTOR ( 'NONE', #3666, 1000.000000000000000 ) ;
#509=ORIENTED_EDGE ( 'NONE', *, *, #5643, .T. ) ;
#512=VECTOR ( 'NONE', #266, 1000.000000000000000 ) ;
#520=CARTESIAN_POINT ( 'NONE',  ( -63.59768876112976699, -218.0630244767148440, 79.13514301043191779 ) ) ;
#521=ORIENTED_EDGE ( 'NONE', *, *, #522, .F. ) ;
#522=EDGE_CURVE ( 'NONE', #7372, #2111, #1110, .T. ) ;
#534=EDGE_LOOP ( 'NONE', ( #5685, #2959, #6105, #5271 ) ) ;
#542=CARTESIAN_POINT ( 'NONE',  ( -34.49999999999998579, 16.00000000000004263, 44.76505905230376925 ) ) ;
#545=AXIS2_PLACEMENT_3D ( 'NONE', #2606, #4420, #913 ) ;
#561=EDGE_CURVE ( 'NONE', #1433, #7339, #6703, .T. ) ;
#572=CARTESIAN_POINT ( 'NONE',  ( -30.49999999999999289, -218.0630240738404950, 71.94153218116483117 ) ) ;
#580=VERTEX_POINT ( 'NONE', #6440 ) ;
#582=LINE ( 'NONE', #1735, #4476 ) ;
#589=VERTEX_POINT ( 'NONE', #5133 ) ;
#592=DIRECTION ( 'NONE',  ( 0.000000000000000000, 0.000000000000000000, 1.000000000000000000 ) ) ;
#605=ORIENTED_EDGE ( 'NONE', *, *, #3368, .F. ) ;
#607=PLANE ( 'NONE',  #1074 ) ;
#613=CARTESIAN_POINT ( 'NONE',  ( -70.24881022415654286, -216.1672007404107489, 77.37948953034242550 ) ) ;
#627=CARTESIAN_POINT ( 'NONE',  ( -21.50000000000000000, -215.0630240738404950, 71.13768460387149162 ) ) ;
#651=CARTESIAN_POINT ( 'NONE',  ( -60.72636667137881972, -221.3248423084427543, 72.81553374298034953 ) ) ;
#655=( BOUNDED_CURVE ( )  B_SPLINE_CURVE ( 3, ( #4048, #6313, #6927, #1729 ),
 .UNSPECIFIED., .F., .T. ) 
 B_SPLINE_CURVE_WITH_KNOTS ( ( 4, 4 ),
 ( 1.570796326794896558, 2.443460952792054108 ),
 .UNSPECIFIED. ) 
 CURVE ( )  GEOMETRIC_REPRESENTATION_ITEM ( )  RATIONAL_B_SPLINE_CURVE ( ( 1.000000000000000000, 0.9375385246911008830, 0.9375385246911008830, 1.000000000000000000 ) ) 
 REPRESENTATION_ITEM ( '' )  );
#679=DIRECTION ( 'NONE',  ( 0.000000000000000000, 0.000000000000000000, -1.000000000000000000 ) ) ;
#691=ORIENTED_EDGE ( 'NONE', *, *, #5164, .T. ) ;
#692=CARTESIAN_POINT ( 'NONE',  ( -60.81252276423130354, -227.0484711946333789, 74.34917548081020300 ) ) ;
#695=CARTESIAN_POINT ( 'NONE',  ( -55.83236997523459166, -218.0620500881349528, 94.91109968007503994 ) ) ;
#696=ORIENTED_EDGE ( 'NONE', *, *, #1553, .F. ) ;
#708=CARTESIAN_POINT ( 'NONE',  ( -20.06899017871461410, -73.43085575620199279, 46.43085575620209227 ) ) ;
#709=LINE ( 'NONE', #4292, #2595 ) ;
#716=FACE_OUTER_BOUND ( 'NONE', #6253, .T. ) ;
#719=CARTESIAN_POINT ( 'NONE',  ( -21.50000000000000000, -104.1739323729103575, 75.12787131935897378 ) ) ;
#723=CARTESIAN_POINT ( 'NONE',  ( -64.50000000000000000, -49.37258300203047412, 6.000000000000000888 ) ) ;
#730=ORIENTED_EDGE ( 'NONE', *, *, #5176, .F. ) ;
#740=ADVANCED_FACE ( 'NONE', ( #6011 ), #6517, .F. ) ;
#743=( LENGTH_UNIT ( ) NAMED_UNIT ( * ) SI_UNIT ( .MILLI., .METRE. ) );
#745=DIRECTION ( 'NONE',  ( -2.465190328815661892E-32, -1.000000000000000000, -1.193489751472043281E-15 ) ) ;
#749=DIRECTION ( 'NONE',  ( 0.000000000000000000, 0.000000000000000000, 1.000000000000000000 ) ) ;
#753=CARTESIAN_POINT ( 'NONE',  ( -63.79792493780531260, -223.0630240738405234, 80.77363827126067974 ) ) ;
#762=CARTESIAN_POINT ( 'NONE',  ( -60.75187451922244719, -223.0194114314941203, 73.26959217102434252 ) ) ;
#768=CARTESIAN_POINT ( 'NONE',  ( -24.15685424949239746, 16.00000000000004263, 36.34314575050770202 ) ) ;
#774=ORIENTED_EDGE ( 'NONE', *, *, #3349, .F. ) ;
#777=AXIS2_PLACEMENT_3D ( 'NONE', #2319, #3441, #7541 ) ;
#789=CARTESIAN_POINT ( 'NONE',  ( -78.75983027283936622, -69.18339347973480358, -2.816606520265136027 ) ) ;
#792=CARTESIAN_POINT ( 'NONE',  ( -58.19347660815660817, -223.0630240738404666, 74.43406038553092685 ) ) ;
#794=AXIS2_PLACEMENT_3D ( 'NONE', #6001, #34, #5427 ) ;
#799=VECTOR ( 'NONE', #6042, 1000.000000000000000 ) ;
#804=ADVANCED_FACE ( 'NONE', ( #4358 ), #3896, .F. ) ;
#805=CARTESIAN_POINT ( 'NONE',  ( -64.08602328290328387, -218.0612840253216405, 86.88646258543963086 ) ) ;
#806=ORIENTED_EDGE ( 'NONE', *, *, #5424, .T. ) ;
#810=ORIENTED_EDGE ( 'NONE', *, *, #4786, .T. ) ;
#819=AXIS2_PLACEMENT_3D ( 'NONE', #3115, #5468, #2541 ) ;
#820=( NAMED_UNIT ( * ) PLANE_ANGLE_UNIT ( ) SI_UNIT ( $, .RADIAN. ) );
#827=CARTESIAN_POINT ( 'NONE',  ( -63.60807779484393620, -223.0630240738404382, 80.31542455955738546 ) ) ;
#832=ORIENTED_EDGE ( 'NONE', *, *, #4232, .F. ) ;
#856=CARTESIAN_POINT ( 'NONE',  ( -26.83962456033763999, -114.3720785834763660, 42.37207858347651523 ) ) ;
#857=EDGE_LOOP ( 'NONE', ( #2203, #6637 ) ) ;
#862=CARTESIAN_POINT ( 'NONE',  ( -56.86408658970942298, -223.0633023296381907, 73.89250821964630234 ) ) ;
#871=LINE ( 'NONE', #3958, #7326 ) ;
#873=LINE ( 'NONE', #3307, #156 ) ;
#876=ORIENTED_EDGE ( 'NONE', *, *, #2272, .T. ) ;
#879=DIRECTION ( 'NONE',  ( -1.000000000000000000, -2.465190328815661892E-32, 9.244463733058732095E-33 ) ) ;
#880=ORIENTED_EDGE ( 'NONE', *, *, #6910, .F. ) ;
#886=DIRECTION ( 'NONE',  ( 1.000000000000000000, 2.465190328815661892E-32, -9.244463733058732095E-33 ) ) ;
#890=CARTESIAN_POINT ( 'NONE',  ( -53.21539232130206898, -217.2436419687049920, 95.06511182196835819 ) ) ;
#902=CARTESIAN_POINT ( 'NONE',  ( -61.06900945253273960, -223.0630335581889483, 76.52804181849850806 ) ) ;
#913=DIRECTION ( 'NONE',  ( -3.697785493223492838E-32, -0.9659258262890682012, 0.2588190451025208505 ) ) ;
#917=VERTEX_POINT ( 'NONE', #6810 ) ;
#919=CIRCLE ( 'NONE', #6946, 6.000000000000000888 ) ;
#920=VERTEX_POINT ( 'NONE', #1492 ) ;
#929=CYLINDRICAL_SURFACE ( 'NONE', #2510, 6.000000000000000888 ) ;
#935=CARTESIAN_POINT ( 'NONE',  ( -21.50000000000000000, 0.000000000000000000, 0.000000000000000000 ) ) ;
#937=ORIENTED_EDGE ( 'NONE', *, *, #3868, .F. ) ;
#940=DIRECTION ( 'NONE',  ( -1.000000000000000000, -4.437342591868191405E-31, 3.379803290564627108E-16 ) ) ;
#944=CARTESIAN_POINT ( 'NONE',  ( -57.82488719026880375, -223.0630234060879218, 95.18029550329626431 ) ) ;
#947=CARTESIAN_POINT ( 'NONE',  ( -57.33489972660768075, -218.0629586075543500, 94.42960329959574040 ) ) ;
#956=ORIENTED_EDGE ( 'NONE', *, *, #2095, .T. ) ;
#961=ADVANCED_BREP_SHAPE_REPRESENTATION ( '', ( #3747, #1914 ), #6207 ) ;
#964=CARTESIAN_POINT ( 'NONE',  ( -24.49999999999998934, 16.00000000000007105, 32.26953873476009704 ) ) ;
#968=CARTESIAN_POINT ( 'NONE',  ( -69.99135978879996856, -225.2480063162100521, 90.90573154067853068 ) ) ;
#970=LINE ( 'NONE', #2820, #3075 ) ;
#973=EDGE_LOOP ( 'NONE', ( #1077, #6732, #1517, #7077 ) ) ;
#978=FACE_OUTER_BOUND ( 'NONE', #100, .T. ) ;
#980=LINE ( 'NONE', #6833, #4423 ) ;
#981=CARTESIAN_POINT ( 'NONE',  ( -61.13443983231169199, -218.0630240738405803, 75.38912616118008714 ) ) ;
#992=AXIS2_PLACEMENT_3D ( 'NONE', #3172, #2091, #2589 ) ;
#998=ORIENTED_EDGE ( 'NONE', *, *, #2075, .F. ) ;
#1003=DIRECTION ( 'NONE',  ( 0.000000000000000000, 1.301042606982607490E-15, -1.000000000000000000 ) ) ;
#1004=PLANE ( 'NONE',  #5223 ) ;
#1007=AXIS2_PLACEMENT_3D ( 'NONE', #3889, #4927, #6222 ) ;
#1008=CARTESIAN_POINT ( 'NONE',  ( -70.03121585365657609, -223.4569485227349048, 90.54948733812102546 ) ) ;
#1010=FACE_OUTER_BOUND ( 'NONE', #6165, .T. ) ;
#1017=DIRECTION ( 'NONE',  ( 1.000000000000000000, 2.465190328815661892E-32, -9.244463733058732095E-33 ) ) ;
#1020=CARTESIAN_POINT ( 'NONE',  ( -57.57279687405196711, -218.0630326314025638, 72.90762633068793264 ) ) ;
#1025=CARTESIAN_POINT ( 'NONE',  ( -53.25759302228803449, -223.0630240738404950, 73.28127814332044920 ) ) ;
#1042=VECTOR ( 'NONE', #104, 1000.000000000000000 ) ;
#1045=CARTESIAN_POINT ( 'NONE',  ( -64.50000000000000000, -49.37258300203047412, 0.000000000000000000 ) ) ;
#1048=CARTESIAN_POINT ( 'NONE',  ( -60.83418965632455411, -223.7273137069676352, 96.20835808347010243 ) ) ;
#1053=EDGE_CURVE ( 'NONE', #7540, #4517, #655, .T. ) ;
#1057=CARTESIAN_POINT ( 'NONE',  ( -63.73162345571661547, -223.0630236663108406, 88.95209687383599828 ) ) ;
#1060=CARTESIAN_POINT ( 'NONE',  ( -61.70062949845839029, -218.0632753655198712, 76.01051187978914925 ) ) ;
#1063=ORIENTED_EDGE ( 'NONE', *, *, #522, .T. ) ;
#1068=CYLINDRICAL_SURFACE ( 'NONE', #270, 6.000000000000000888 ) ;
#1071=VERTEX_POINT ( 'NONE', #6849 ) ;
#1072=EDGE_CURVE ( 'NONE', #1754, #228, #2592, .T. ) ;
#1074=AXIS2_PLACEMENT_3D ( 'NONE', #7225, #4233, #3694 ) ;
#1077=ORIENTED_EDGE ( 'NONE', *, *, #6155, .T. ) ;
#1093=CARTESIAN_POINT ( 'NONE',  ( -64.50000000000000000, -125.0933926253236450, 30.46597562735434295 ) ) ;
#1095=CARTESIAN_POINT ( 'NONE',  ( -21.49999999999999645, -69.31370849898463860, 42.31370849898474518 ) ) ;
#1096=CARTESIAN_POINT ( 'NONE',  ( -64.48423350399045262, -218.0630240738404666, 82.51610664137940887 ) ) ;
#1106=CIRCLE ( 'NONE', #6024, 6.000000000000000000 ) ;
#1110=CIRCLE ( 'NONE', #992, 7.999999999999986677 ) ;
#1121=ORIENTED_EDGE ( 'NONE', *, *, #196, .F. ) ;
#1135=EDGE_LOOP ( 'NONE', ( #7223, #3118, #6738, #2764, #1706 ) ) ;
#1139=CARTESIAN_POINT ( 'NONE',  ( -64.50000000000000000, -49.37258300203047412, 0.000000000000000000 ) ) ;
#1141=EDGE_CURVE ( 'NONE', #917, #3477, #3779, .T. ) ;
#1142=ORIENTED_EDGE ( 'NONE', *, *, #4689, .T. ) ;
#1146=CARTESIAN_POINT ( 'NONE',  ( -53.40199052334469343, -221.4565245236473174, 95.80795668296072165 ) ) ;
#1149=DIRECTION ( 'NONE',  ( 0.000000000000000000, 0.000000000000000000, -1.000000000000000000 ) ) ;
#1156=DIRECTION ( 'NONE',  ( -3.081487911019577365E-33, -1.193489751472043281E-15, 1.000000000000000000 ) ) ;
#1164=VERTEX_POINT ( 'NONE', #1882 ) ;
#1170=LINE ( 'NONE', #2938, #1042 ) ;
#1175=PRODUCT_DEFINITION_CONTEXT ( 'detailed design', #3096, 'design' ) ;
#1176=EDGE_CURVE ( 'NONE', #4666, #1433, #5357, .T. ) ;
#1186=AXIS2_PLACEMENT_3D ( 'NONE', #2671, #940, #4954 ) ;
#1189=CARTESIAN_POINT ( 'NONE',  ( -60.76462208873361703, -223.8662738488898754, 73.49650827185847390 ) ) ;
#1193=EDGE_LOOP ( 'NONE', ( #3110, #1759, #4270, #321, #6307, #2770, #3810, #4304, #5974, #5075, #3253, #4830 ) ) ;
#1213=ORIENTED_EDGE ( 'NONE', *, *, #6472, .F. ) ;
#1228=CARTESIAN_POINT ( 'NONE',  ( -70.21559789597881718, -215.1711607728661022, 88.90143116695425363 ) ) ;
#1236=EDGE_LOOP ( 'NONE', ( #3768, #6263, #4015, #282, #7066, #1569, #1565, #730, #774, #4230 ) ) ;
#1242=ADVANCED_FACE ( 'NONE', ( #4965 ), #2038, .F. ) ;
#1251=UNCERTAINTY_MEASURE_WITH_UNIT (LENGTH_MEASURE( 1.000000000000000082E-05 ), #4876, 'distance_accuracy_value', 'NONE');
#1253=CARTESIAN_POINT ( 'NONE',  ( -64.50000000000000000, -223.0630240738404950, 96.09122589815579829 ) ) ;
#1258=DIRECTION ( 'NONE',  ( 1.000000000000000000, 2.465190328815661892E-32, -9.244463733058732095E-33 ) ) ;
#1263=CARTESIAN_POINT ( 'NONE',  ( -29.64230087749237086, -110.3978942797115650, 38.39789427971174263 ) ) ;
#1265=CARTESIAN_POINT ( 'NONE',  ( -53.33013951010422460, -224.6695236240153122, 73.71173840043080361 ) ) ;
#1267=CARTESIAN_POINT ( 'NONE',  ( -56.20284895707440143, -218.0622243524431667, 94.81566216203397346 ) ) ;
#1287=CARTESIAN_POINT ( 'NONE',  ( -27.57070108872857617, -112.5545107178312350, 40.55451071783139128 ) ) ;
#1293=ORIENTED_EDGE ( 'NONE', *, *, #6624, .F. ) ;
#1295=CARTESIAN_POINT ( 'NONE',  ( -26.49999999999999289, -214.0630240738404382, 71.94153218116485959 ) ) ;
#1299=ADVANCED_FACE ( 'NONE', ( #6640 ), #3569, .F. ) ;
#1303=CARTESIAN_POINT ( 'NONE',  ( -53.25168462842736261, -218.0630240738404950, 95.20959099461346398 ) ) ;
#1304=CARTESIAN_POINT ( 'NONE',  ( -53.21539232130207608, -222.1285142276788065, 73.03087698472252498 ) ) ;
#1308=CARTESIAN_POINT ( 'NONE',  ( -63.70092059630563597, -218.0630238739302627, 87.96661164443882797 ) ) ;
#1315=DIRECTION ( 'NONE',  ( 0.000000000000000000, -1.000000000000000000, 0.000000000000000000 ) ) ;
#1316=CARTESIAN_POINT ( 'NONE',  ( -34.49999999999998579, -218.0630240738404382, 44.76505905230349214 ) ) ;
#1330=CARTESIAN_POINT ( 'NONE',  ( -63.60391380032690023, -223.0630241410106578, 80.30539155062909629 ) ) ;
#1332=ORIENTED_EDGE ( 'NONE', *, *, #3954, .T. ) ;
#1337=CARTESIAN_POINT ( 'NONE',  ( -53.40199052334512686, -226.2606222968797169, 74.13807200490302307 ) ) ;
#1339=CARTESIAN_POINT ( 'NONE',  ( -64.45762304774287088, -218.0620869872676622, 84.71565845322002986 ) ) ;
#1352=EDGE_CURVE ( 'NONE', #2966, #5372, #6482, .T. ) ;
#1365=CARTESIAN_POINT ( 'NONE',  ( -57.26052226718441318, -223.0630848540440923, 74.04027840652977943 ) ) ;
#1370=LINE ( 'NONE', #723, #4017 ) ;
#1375=CARTESIAN_POINT ( 'NONE',  ( -61.19496864977951134, -218.0630138500335704, 91.85947964960436707 ) ) ;
#1379=CARTESIAN_POINT ( 'NONE',  ( -25.67719663180530176, -106.8228033681944993, 34.82280336819465560 ) ) ;
#1383=LINE ( 'NONE', #3748, #3879 ) ;
#1388=ORIENTED_EDGE ( 'NONE', *, *, #6838, .F. ) ;
#1393=CARTESIAN_POINT ( 'NONE',  ( -26.49999999999998934, -223.0630240738404950, 96.09122589815579829 ) ) ;
#1395=ADVANCED_FACE ( 'NONE', ( #6567 ), #5416, .T. ) ;
#1397=VERTEX_POINT ( 'NONE', #7398 ) ;
#1399=AXIS2_PLACEMENT_3D ( 'NONE', #5362, #3634, #5973 ) ;
#1409=( BOUNDED_CURVE ( )  B_SPLINE_CURVE ( 3, ( #7226, #6761, #4307, #5503 ),
 .UNSPECIFIED., .F., .T. ) 
 B_SPLINE_CURVE_WITH_KNOTS ( ( 4, 4 ),
 ( 1.637599047967247534, 2.356194490192342172 ),
 .UNSPECIFIED. ) 
 CURVE ( )  GEOMETRIC_REPRESENTATION_ITEM ( )  RATIONAL_B_SPLINE_CURVE ( ( 1.000000000000000000, 0.9574293250827445867, 0.9574293250827445867, 1.000000000000000000 ) ) 
 REPRESENTATION_ITEM ( '' )  );
#1413=VERTEX_POINT ( 'NONE', #2594 ) ;
#1416=CARTESIAN_POINT ( 'NONE',  ( -21.50000000000000000, -99.90626354475344328, 72.90626354475362803 ) ) ;
#1419=CARTESIAN_POINT ( 'NONE',  ( -56.93191179421732073, -218.0627243648279716, 94.58151066868406076 ) ) ;
#1433=VERTEX_POINT ( 'NONE', #6717 ) ;
#1442=EDGE_CURVE ( 'NONE', #580, #5543, #6223, .T. ) ;
#1445=CARTESIAN_POINT ( 'NONE',  ( -64.44976119587670382, -223.0636454045093444, 83.68982568666081079 ) ) ;
#1462=DIRECTION ( 'NONE',  ( 0.000000000000000000, 0.000000000000000000, 1.000000000000000000 ) ) ;
#1466=CARTESIAN_POINT ( 'NONE',  ( -60.83909347413332114, -224.0594585235270415, 96.26692417614295039 ) ) ;
#1476=CARTESIAN_POINT ( 'NONE',  ( -57.52121243805820683, -223.0630252886708149, 74.14711318252129502 ) ) ;
#1480=ORIENTED_EDGE ( 'NONE', *, *, #4608, .T. ) ;
#1483=CYLINDRICAL_SURFACE ( 'NONE', #5859, 7.999999999999986677 ) ;
#1484=CARTESIAN_POINT ( 'NONE',  ( -26.49999999999999289, -99.90626354475344328, 72.90626354475362803 ) ) ;
#1488=ORIENTED_EDGE ( 'NONE', *, *, #5889, .F. ) ;
#1492=CARTESIAN_POINT ( 'NONE',  ( -23.84314575050760965, -108.6568542494922127, 36.65685424949233351 ) ) ;
#1493=FACE_OUTER_BOUND ( 'NONE', #5067, .T. ) ;
#1498=DIRECTION ( 'NONE',  ( 1.000000000000000000, 1.725633230170963324E-31, -1.078147950931789757E-16 ) ) ;
#1502=CARTESIAN_POINT ( 'NONE',  ( -32.50000000000002132, -61.67366827531365914, 34.67366827531376572 ) ) ;
#1503=B_SPLINE_CURVE_WITH_KNOTS ( 'NONE', 3,
 ( #4814, #3148, #4923, #6727, #3886, #6299, #3304, #1025 ),
 .UNSPECIFIED., .F., .F.,
 ( 4, 2, 2, 4 ),
 ( 0.000000000000000000, 0.4916292630627406846, 0.9738324145908705542, 1.000000000000000000 ),
 .UNSPECIFIED. ) ;
#1504=VECTOR ( 'NONE', #4058, 1000.000000000000000 ) ;
#1512=CARTESIAN_POINT ( 'NONE',  ( -56.37211203147379734, -223.0620538650801734, 95.72315438295314038 ) ) ;
#1517=ORIENTED_EDGE ( 'NONE', *, *, #6838, .T. ) ;
#1535=CYLINDRICAL_SURFACE ( 'NONE', #6194, 8.000000000000028422 ) ;
#1538=CARTESIAN_POINT ( 'NONE',  ( -32.50000000000002132, 16.00000000000006750, 32.26953873476009704 ) ) ;
#1541=CARTESIAN_POINT ( 'NONE',  ( -64.50000000000000000, -39.68629150101521219, 24.00000000000002132 ) ) ;
#1552=CARTESIAN_POINT ( 'NONE',  ( -59.34588541462897382, -223.0624788587527974, 94.37260828691398729 ) ) ;
#1553=EDGE_CURVE ( 'NONE', #5460, #4643, #3177, .T. ) ;
#1556=CARTESIAN_POINT ( 'NONE',  ( -53.03180245857092956, -218.0630240738404950, 71.94153218116483117 ) ) ;
#1564=DIRECTION ( 'NONE',  ( 0.000000000000000000, 0.000000000000000000, -1.000000000000000000 ) ) ;
#1565=ORIENTED_EDGE ( 'NONE', *, *, #5164, .F. ) ;
#1569=ORIENTED_EDGE ( 'NONE', *, *, #5977, .T. ) ;
#1571=CARTESIAN_POINT ( 'NONE',  ( -21.50000000000000355, -114.1489496936987962, 42.14012972382754185 ) ) ;
#1578=FACE_OUTER_BOUND ( 'NONE', #6743, .T. ) ;
#1580=CARTESIAN_POINT ( 'NONE',  ( -26.69871789691343267, -115.0146905589846540, 42.92178193144403764 ) ) ;
#1582=ORIENTED_EDGE ( 'NONE', *, *, #4608, .F. ) ;
#1588=CARTESIAN_POINT ( 'NONE',  ( -57.92294587369016767, -223.0630151802142223, 95.13692867617221793 ) ) ;
#1591=CARTESIAN_POINT ( 'NONE',  ( -64.50037575164097348, -218.0629762364925170, 83.76610889236388857 ) ) ;
#1597=DIRECTION ( 'NONE',  ( 4.930380657631324879E-32, 0.9659258262890683122, -0.2588190451025207950 ) ) ;
#1600=CARTESIAN_POINT ( 'NONE',  ( -26.50000000000003197, -57.68629150101511271, 30.68629150101523351 ) ) ;
#1613=DIRECTION ( 'NONE',  ( -2.465190328815661892E-32, -1.000000000000000000, -1.193489751472043281E-15 ) ) ;
#1618=CARTESIAN_POINT ( 'NONE',  ( -53.33013951010422460, -219.8343230396700392, 95.52191879319023826 ) ) ;
#1626=CARTESIAN_POINT ( 'NONE',  ( -59.03668131115762918, -223.0625876205039901, 94.56341339751826069 ) ) ;
#1630=CARTESIAN_POINT ( 'NONE',  ( -59.02881190857226557, -218.0635488414859537, 73.67786969443412204 ) ) ;
#1640=CIRCLE ( 'NONE', #5580, 15.99999999999999645 ) ;
#1648=VECTOR ( 'NONE', #6449, 1000.000000000000000 ) ;
#1659=EDGE_LOOP ( 'NONE', ( #7277, #7011, #5192, #3270, #880, #2428, #6969, #4161 ) ) ;
#1674=DIRECTION ( 'NONE',  ( 1.000000000000000000, 2.465190328815661892E-32, -9.244463733058732095E-33 ) ) ;
#1675=DIRECTION ( 'NONE',  ( -1.000000000000000000, -1.725633230170963324E-31, 1.078147950931789387E-16 ) ) ;
#1677=CARTESIAN_POINT ( 'NONE',  ( -54.49733181648158364, -218.0639264276503297, 72.01289010251366562 ) ) ;
#1694=DIRECTION ( 'NONE',  ( -1.000000000000000000, -2.465190328815661892E-32, 9.244463733058732095E-33 ) ) ;
#1695=LINE ( 'NONE', #3626, #5593 ) ;
#1697=ORIENTED_EDGE ( 'NONE', *, *, #196, .T. ) ;
#1706=ORIENTED_EDGE ( 'NONE', *, *, #3822, .T. ) ;
#1720=CIRCLE ( 'NONE', #4426, 7.999999999999986677 ) ;
#1725=FACE_OUTER_BOUND ( 'NONE', #5005, .T. ) ;
#1729=CARTESIAN_POINT ( 'NONE',  ( -29.35769912250765046, -65.63670350735181103, 38.63670350735190340 ) ) ;
#1734=ORIENTED_EDGE ( 'NONE', *, *, #4763, .F. ) ;
#1735=CARTESIAN_POINT ( 'NONE',  ( -21.50000000000000000, -215.0630240738403813, -2.775557561562891351E-13 ) ) ;
#1749=CARTESIAN_POINT ( 'NONE',  ( 0.000000000000000000, 0.000000000000000000, 0.000000000000000000 ) ) ;
#1754=VERTEX_POINT ( 'NONE', #6597 ) ;
#1759=ORIENTED_EDGE ( 'NONE', *, *, #7005, .F. ) ;
#1768=CARTESIAN_POINT ( 'NONE',  ( -52.98766809822285495, -217.0856944719845671, 71.67965750360849597 ) ) ;
#1778=ORIENTED_EDGE ( 'NONE', *, *, #2042, .F. ) ;
#1802=DIRECTION ( 'NONE',  ( 7.623657272262514668E-17, -0.7071067811865465735, 0.7071067811865485719 ) ) ;
#1804=VECTOR ( 'NONE', #1597, 1000.000000000000114 ) ;
#1811=CARTESIAN_POINT ( 'NONE',  ( -70.14230383934500423, -220.9072961629242968, 78.53943569403833180 ) ) ;
#1825=CARTESIAN_POINT ( 'NONE',  ( -32.50000000000002842, -49.37258300203047412, 0.000000000000000000 ) ) ;
#1831=DIRECTION ( 'NONE',  ( 4.930380657631323236E-32, 0.9848077530122080203, -0.1736481776669304422 ) ) ;
#1833=CARTESIAN_POINT ( 'NONE',  ( -26.50000000000003197, -49.37258300203047412, 6.000000000000002665 ) ) ;
#1841=CARTESIAN_POINT ( 'NONE',  ( -64.50000000000000000, 0.000000000000000000, 0.000000000000000000 ) ) ;
#1843=VERTEX_POINT ( 'NONE', #4140 ) ;
#1845=CARTESIAN_POINT ( 'NONE',  ( -70.08493024494319457, -221.0431231857560306, 90.06937369499782164 ) ) ;
#1847=CARTESIAN_POINT ( 'NONE',  ( -63.69261809097343274, -218.0630232800231738, 87.98794966951278695 ) ) ;
#1850=ORIENTED_EDGE ( 'NONE', *, *, #4624, .F. ) ;
#1858=DIRECTION ( 'NONE',  ( -2.465190328815662439E-32, -0.7071067811865464625, 0.7071067811865485719 ) ) ;
#1863=DIRECTION ( 'NONE',  ( 3.081487911019577365E-33, 1.193489751472043281E-15, -1.000000000000000000 ) ) ;
#1864=DIRECTION ( 'NONE',  ( 1.000000000000000000, 0.000000000000000000, 0.000000000000000000 ) ) ;
#1870=EDGE_CURVE ( 'NONE', #580, #5858, #5156, .T. ) ;
#1880=CARTESIAN_POINT ( 'NONE',  ( -70.16044999292957129, -217.6494054747795417, 89.39435792273813775 ) ) ;
#1882=CARTESIAN_POINT ( 'NONE',  ( -26.50000000000002842, -49.37258300203047412, -16.00000000000004263 ) ) ;
#1886=AXIS2_PLACEMENT_3D ( 'NONE', #1093, #1017, #4490 ) ;
#1897=AXIS2_PLACEMENT_3D ( 'NONE', #1841, #4199, #6544 ) ;
#1898=AXIS2_PLACEMENT_3D ( 'NONE', #1825, #6373, #592 ) ;
#1913=CARTESIAN_POINT ( 'NONE',  ( -63.46819182528941639, -223.0630670020534296, 79.98999288546480102 ) ) ;
#1914=AXIS2_PLACEMENT_3D ( 'NONE', #1749, #62, #1864 ) ;
#1922=CARTESIAN_POINT ( 'NONE',  ( -70.00607124224620748, -226.9703646923684914, 80.02312588464759813 ) ) ;
#1925=CARTESIAN_POINT ( 'NONE',  ( -64.32060244815615135, -218.0610728454553850, 85.77987718927815308 ) ) ;
#1929=AXIS2_PLACEMENT_3D ( 'NONE', #1253, #70, #1831 ) ;
#1948=CARTESIAN_POINT ( 'NONE',  ( -63.76541543211998686, -223.0629989142765339, 88.86326335188097403 ) ) ;
#1954=EDGE_CURVE ( 'NONE', #4795, #7371, #4395, .T. ) ;
#1963=FACE_OUTER_BOUND ( 'NONE', #61, .T. ) ;
#1965=EDGE_CURVE ( 'NONE', #2388, #5372, #4122, .T. ) ;
#1971=DIRECTION ( 'NONE',  ( 1.000000000000000000, 2.465190328815661892E-32, -9.244463733058732095E-33 ) ) ;
#1984=CARTESIAN_POINT ( 'NONE',  ( -57.54473169771259933, -223.0630240738405234, 74.15707378103115843 ) ) ;
#1989=ORIENTED_EDGE ( 'NONE', *, *, #3544, .F. ) ;
#1991=VECTOR ( 'NONE', #5751, 1000.000000000000000 ) ;
#1996=CARTESIAN_POINT ( 'NONE',  ( -63.67592485445254624, -218.0630209448846699, 88.03053438521520491 ) ) ;
#1999=ORIENTED_EDGE ( 'NONE', *, *, #4689, .F. ) ;
#2000=AXIS2_PLACEMENT_3D ( 'NONE', #5367, #5207, #1858 ) ;
#2001=LINE ( 'NONE', #6808, #7182 ) ;
#2017=EDGE_LOOP ( 'NONE', ( #3414, #5671, #2424, #3659 ) ) ;
#2025=CARTESIAN_POINT ( 'NONE',  ( -54.69181398302472275, -223.0639029778887448, 73.35099609428758072 ) ) ;
#2035=FACE_OUTER_BOUND ( 'NONE', #3316, .T. ) ;
#2038=PLANE ( 'NONE',  #819 ) ;
#2041=ORIENTED_EDGE ( 'NONE', *, *, #6801, .T. ) ;
#2042=EDGE_CURVE ( 'NONE', #2908, #1843, #6367, .T. ) ;
#2047=CARTESIAN_POINT ( 'NONE',  ( -32.50000000000002842, -49.37258300203047412, 0.000000000000000000 ) ) ;
#2048=LINE ( 'NONE', #7280, #4234 ) ;
#2063=CARTESIAN_POINT ( 'NONE',  ( -61.64566566670315240, -223.0630240738406371, 77.11548722274392276 ) ) ;
#2074=B_SPLINE_CURVE_WITH_KNOTS ( 'NONE', 3,
 ( #6711, #856, #1580, #3445, #6860, #3979 ),
 .UNSPECIFIED., .F., .F.,
 ( 4, 2, 4 ),
 ( 0.000000000000000000, 0.002568044547241839747, 0.005136089094483679493 ),
 .UNSPECIFIED. ) ;
#2075=EDGE_CURVE ( 'NONE', #2971, #2880, #6728, .T. ) ;
#2084=( GEOMETRIC_REPRESENTATION_CONTEXT ( 3 ) GLOBAL_UNCERTAINTY_ASSIGNED_CONTEXT ( ( #1251 ) ) GLOBAL_UNIT_ASSIGNED_CONTEXT ( ( #4876, #5601, #325 ) ) REPRESENTATION_CONTEXT ( 'NONE', 'WORKASPACE' ) );
#2089=CARTESIAN_POINT ( 'NONE',  ( -53.00237955168282866, -212.4343899438498795, 94.21711093295959927 ) ) ;
#2091=DIRECTION ( 'NONE',  ( -1.000000000000000000, -2.465190328815661892E-32, 9.244463733058732095E-33 ) ) ;
#2095=EDGE_CURVE ( 'NONE', #3503, #4666, #4613, .T. ) ;
#2101=LINE ( 'NONE', #3107, #7370 ) ;
#2102=ORIENTED_EDGE ( 'NONE', *, *, #1965, .T. ) ;
#2111=VERTEX_POINT ( 'NONE', #7572 ) ;
#2112=CIRCLE ( 'NONE', #30, 6.000000000000000888 ) ;
#2113=ADVANCED_FACE ( 'NONE', ( #3545, #4664, #1725 ), #607, .F. ) ;
#2124=DIRECTION ( 'NONE',  ( 1.000000000000000000, 2.465190328815661892E-32, -9.244463733058732095E-33 ) ) ;
#2134=CYLINDRICAL_SURFACE ( 'NONE', #1886, 15.99999999999997335 ) ;
#2138=CARTESIAN_POINT ( 'NONE',  ( -57.71305776231798745, -218.0630565819627122, 72.97053707171922099 ) ) ;
#2140=VECTOR ( 'NONE', #7433, 1000.000000000000000 ) ;
#2142=EDGE_LOOP ( 'NONE', ( #7174, #4482 ) ) ;
#2143=ORIENTED_EDGE ( 'NONE', *, *, #4275, .T. ) ;
#2145=LINE ( 'NONE', #5006, #1804 ) ;
#2155=VERTEX_POINT ( 'NONE', #7150 ) ;
#2156=DIRECTION ( 'NONE',  ( 1.000000000000000000, 2.465190328815661892E-32, -9.244463733058732095E-33 ) ) ;
#2165=LINE ( 'NONE', #1538, #5589 ) ;
#2168=CARTESIAN_POINT ( 'NONE',  ( -69.99871551551754578, -224.9174535703052413, 90.83998408137780700 ) ) ;
#2170=LINE ( 'NONE', #3908, #2262 ) ;
#2174=VERTEX_POINT ( 'NONE', #1416 ) ;
#2178=CARTESIAN_POINT ( 'NONE',  ( -63.72797457321117776, -223.0630240738404950, 88.96157793287162008 ) ) ;
#2180=CARTESIAN_POINT ( 'NONE',  ( -26.49999999999999645, -214.0630240738404666, 70.86973541144037370 ) ) ;
#2181=CARTESIAN_POINT ( 'NONE',  ( -61.17656753709511008, -218.0630265158296481, 75.43246580923499778 ) ) ;
#2199=EDGE_CURVE ( 'NONE', #7371, #7274, #1370, .T. ) ;
#2203=ORIENTED_EDGE ( 'NONE', *, *, #7493, .F. ) ;
#2205=DIRECTION ( 'NONE',  ( 0.000000000000000000, 0.000000000000000000, 1.000000000000000000 ) ) ;
#2218=CARTESIAN_POINT ( 'NONE',  ( -57.80716452887639178, -223.0630240738405803, 95.18803987619344298 ) ) ;
#2221=CARTESIAN_POINT ( 'NONE',  ( -62.88741732078067770, -218.0636600088369050, 77.64984730018771586 ) ) ;
#2240=DIRECTION ( 'NONE',  ( -2.465190328815661892E-32, -0.7071067811865465735, 0.7071067811865484609 ) ) ;
#2249=CARTESIAN_POINT ( 'NONE',  ( -60.68960140267979853, -213.9340789708222133, 94.48154657109718357 ) ) ;
#2252=EDGE_CURVE ( 'NONE', #7513, #3412, #1503, .T. ) ;
#2260=CARTESIAN_POINT ( 'NONE',  ( -64.50055673519366906, -218.0630240738405803, 83.63996444840225308 ) ) ;
#2262=VECTOR ( 'NONE', #439, 1000.000000000000000 ) ;
#2272=EDGE_CURVE ( 'NONE', #4080, #1754, #2145, .T. ) ;
#2274=EDGE_LOOP ( 'NONE', ( #2930, #6780 ) ) ;
#2302=EDGE_LOOP ( 'NONE', ( #7340, #5160, #6963, #458 ) ) ;
#2314=EDGE_CURVE ( 'NONE', #4517, #2475, #871, .T. ) ;
#2319=CARTESIAN_POINT ( 'NONE',  ( -32.50000000000002842, 6.938893903907228378E-15, 0.000000000000000000 ) ) ;
#2323=CARTESIAN_POINT ( 'NONE',  ( -26.49999999999998934, -214.0630240738404666, 94.50428307177961074 ) ) ;
#2335=DIRECTION ( 'NONE',  ( 3.081487911019577365E-33, 1.193489751472043281E-15, -1.000000000000000000 ) ) ;
#2343=ORIENTED_EDGE ( 'NONE', *, *, #4772, .F. ) ;
#2346=CARTESIAN_POINT ( 'NONE',  ( -32.50000000000002842, 0.000000000000000000, -15.99999999999998579 ) ) ;
#2366=LINE ( 'NONE', #2442, #1648 ) ;
#2373=CARTESIAN_POINT ( 'NONE',  ( -29.35769912250765046, -110.6367035073516831, 38.63670350735182524 ) ) ;
#2375=ADVANCED_FACE ( 'NONE', ( #2035 ), #1483, .T. ) ;
#2380=CARTESIAN_POINT ( 'NONE',  ( -64.50000000000000000, 0.000000000000000000, 6.000000000000000000 ) ) ;
#2381=AXIS2_PLACEMENT_3D ( 'NONE', #542, #4018, #1003 ) ;
#2388=VERTEX_POINT ( 'NONE', #4456 ) ;
#2401=ORIENTED_EDGE ( 'NONE', *, *, #2272, .F. ) ;
#2420=ORIENTED_EDGE ( 'NONE', *, *, #336, .F. ) ;
#2423=CARTESIAN_POINT ( 'NONE',  ( -53.43756829269515407, -222.2597742987333334, 95.94959129055638414 ) ) ;
#2424=ORIENTED_EDGE ( 'NONE', *, *, #7381, .T. ) ;
#2425=CARTESIAN_POINT ( 'NONE',  ( -53.43756829269602804, -227.0484711946323841, 74.34917548081359939 ) ) ;
#2428=ORIENTED_EDGE ( 'NONE', *, *, #2677, .T. ) ;
#2442=CARTESIAN_POINT ( 'NONE',  ( -26.50000000000000355, 16.00000000000004263, 44.76505905230376925 ) ) ;
#2450=FACE_OUTER_BOUND ( 'NONE', #3737, .T. ) ;
#2460=CARTESIAN_POINT ( 'NONE',  ( -70.19709702122540307, -216.0025558445558431, 89.06679694989070128 ) ) ;
#2462=CARTESIAN_POINT ( 'NONE',  ( -60.16175026646936885, -218.0625557288923062, 92.79915306242389761 ) ) ;
#2475=VERTEX_POINT ( 'NONE', #2373 ) ;
#2479=CARTESIAN_POINT ( 'NONE',  ( -32.50000000000002132, -59.26953873475993362, 32.26953873476001888 ) ) ;
#2480=DIRECTION ( 'NONE',  ( 1.000000000000000000, 2.465190328815661892E-32, -9.244463733058732095E-33 ) ) ;
#2487=CARTESIAN_POINT ( 'NONE',  ( -60.62854973486462029, -223.0631873914031473, 76.11203873288630462 ) ) ;
#2495=CARTESIAN_POINT ( 'NONE',  ( -53.51728042240002026, -228.8136496942592828, 74.82215363428539945 ) ) ;
#2501=ORIENTED_EDGE ( 'NONE', *, *, #561, .T. ) ;
#2509=CARTESIAN_POINT ( 'NONE',  ( -32.50000000000002132, -104.2695387347598199, 32.26953873475996204 ) ) ;
#2510=AXIS2_PLACEMENT_3D ( 'NONE', #6706, #886, #388 ) ;
#2528=DIRECTION ( 'NONE',  ( 0.6444004775717536715, -0.5407162030609466985, 0.5407162030609483638 ) ) ;
#2530=CARTESIAN_POINT ( 'NONE',  ( -64.49542967829545148, -223.0630240738403813, 84.38699617518491891 ) ) ;
#2539=DIRECTION ( 'NONE',  ( -2.465190328815662439E-32, -1.000000000000000000, 0.000000000000000000 ) ) ;
#2541=DIRECTION ( 'NONE',  ( 1.000000000000000000, 2.465190328815661892E-32, -9.244463733058732095E-33 ) ) ;
#2542=CARTESIAN_POINT ( 'NONE',  ( -60.75147712453755844, -218.0628479320674842, 92.28982506784103634 ) ) ;
#2562=CARTESIAN_POINT ( 'NONE',  ( -63.95077716541958068, -223.0623318094975502, 88.33193110890873356 ) ) ;
#2568=DIRECTION ( 'NONE',  ( 1.000000000000000000, 2.465190328815661892E-32, -9.244463733058732095E-33 ) ) ;
#2573=CARTESIAN_POINT ( 'NONE',  ( -62.21889548225904321, -218.0624042392298634, 90.69967475268330759 ) ) ;
#2579=DIRECTION ( 'NONE',  ( 0.6427876096865583477, 9.159339953157543431E-16, -0.7660444431189621373 ) ) ;
#2589=DIRECTION ( 'NONE',  ( 0.000000000000000000, -8.673617379884050263E-16, -1.000000000000000000 ) ) ;
#2592=CIRCLE ( 'NONE', #5174, 15.99999999999997691 ) ;
#2594=CARTESIAN_POINT ( 'NONE',  ( -53.25168462842736261, -218.0630240738404950, 95.20959099461346398 ) ) ;
#2595=VECTOR ( 'NONE', #6129, 1000.000000000000000 ) ;
#2598=CARTESIAN_POINT ( 'NONE',  ( -59.74328897643390235, -223.0635515775393856, 75.39397519229926559 ) ) ;
#2606=CARTESIAN_POINT ( 'NONE',  ( -64.50000000000000000, -120.9522879036833416, 45.92078884797942351 ) ) ;
#2609=ORIENTED_EDGE ( 'NONE', *, *, #1176, .T. ) ;
#2616=CARTESIAN_POINT ( 'NONE',  ( -29.35769912250765046, 16.00000000000004263, 38.63670350735201708 ) ) ;
#2617=DIRECTION ( 'NONE',  ( -2.465190328815661892E-32, -1.000000000000000000, -1.193489751472043281E-15 ) ) ;
#2623=LINE ( 'NONE', #4256, #4120 ) ;
#2639=CARTESIAN_POINT ( 'NONE',  ( -64.40058489821628029, -223.0610658478785524, 86.48602887601485634 ) ) ;
#2651=ORIENTED_EDGE ( 'NONE', *, *, #2075, .T. ) ;
#2662=FACE_BOUND ( 'NONE', #857, .T. ) ;
#2665=CARTESIAN_POINT ( 'NONE',  ( -60.76462208873360282, -219.0153713307823580, 95.37751551101587211 ) ) ;
#2671=CARTESIAN_POINT ( 'NONE',  ( -26.49999999999999645, -105.5631177942458407, 67.24940929526130162 ) ) ;
#2674=CARTESIAN_POINT ( 'NONE',  ( -64.50000000000000000, 0.000000000000000000, 0.000000000000000000 ) ) ;
#2677=EDGE_CURVE ( 'NONE', #312, #589, #709, .T. ) ;
#2678=EDGE_CURVE ( 'NONE', #2475, #7561, #6668, .T. ) ;
#2700=CARTESIAN_POINT ( 'NONE',  ( -53.10580595754474587, -214.7694783647500856, 94.62885002390424916 ) ) ;
#2710=CARTESIAN_POINT ( 'NONE',  ( -63.43106901615326620, -223.0630240738406087, 89.73152280343640541 ) ) ;
#2713=CARTESIAN_POINT ( 'NONE',  ( -63.02662698389872986, -218.0624813771180470, 89.41762891734713037 ) ) ;
#2716=DIRECTION ( 'NONE',  ( 8.747574602982982877E-17, -0.9659258262890683122, 0.2588190451025209060 ) ) ;
#2728=DIRECTION ( 'NONE',  ( 0.000000000000000000, 1.301042606982600785E-15, -1.000000000000000000 ) ) ;
#2732=CARTESIAN_POINT ( 'NONE',  ( -32.50000000000002132, 16.00000000000006750, 32.26953873476009704 ) ) ;
#2747=CARTESIAN_POINT ( 'NONE',  ( -62.25770276840173523, -223.0625327031958136, 91.64692538425377677 ) ) ;
#2748=DIRECTION ( 'NONE',  ( 1.000000000000000000, 1.725633230170963324E-31, -1.078147950931789387E-16 ) ) ;
#2750=CARTESIAN_POINT ( 'NONE',  ( -63.59392405224133427, -218.0630241027633360, 79.12603136341994059 ) ) ;
#2764=ORIENTED_EDGE ( 'NONE', *, *, #2678, .T. ) ;
#2770=ORIENTED_EDGE ( 'NONE', *, *, #3884, .F. ) ;
#2772=CARTESIAN_POINT ( 'NONE',  ( -21.51784377693468642, -113.7796841263389069, 41.77968412633906325 ) ) ;
#2790=DIRECTION ( 'NONE',  ( 1.000000000000000000, 2.465190328815661892E-32, -9.244463733058732095E-33 ) ) ;
#2793=CARTESIAN_POINT ( 'NONE',  ( -63.78893983331448680, -218.0634842797883550, 79.62726457540794911 ) ) ;
#2800=EDGE_CURVE ( 'NONE', #4118, #7372, #7472, .T. ) ;
#2804=ORIENTED_EDGE ( 'NONE', *, *, #5176, .T. ) ;
#2815=ORIENTED_EDGE ( 'NONE', *, *, #1965, .F. ) ;
#2817=CARTESIAN_POINT ( 'NONE',  ( -53.48785751550376233, -223.3951688904016635, 96.14979199081800232 ) ) ;
#2818=ADVANCED_FACE ( 'NONE', ( #1578 ), #5706, .F. ) ;
#2820=CARTESIAN_POINT ( 'NONE',  ( -13.22915763683106327, -74.27084236316865429, 47.27084236316875376 ) ) ;
#2827=CARTESIAN_POINT ( 'NONE',  ( -64.50000000000000000, -60.68629150101524061, -11.31370849898474873 ) ) ;
#2831=CARTESIAN_POINT ( 'NONE',  ( -61.22733771064481800, -218.0630336083857230, 75.48520206723708270 ) ) ;
#2832=AXIS2_PLACEMENT_3D ( 'NONE', #5320, #96, #1315 ) ;
#2834=CARTESIAN_POINT ( 'NONE',  ( -21.49999999999999645, -219.7493155748557285, 95.50692968358183066 ) ) ;
#2844=CARTESIAN_POINT ( 'NONE',  ( -26.49999999999999645, -214.0630240738404666, 70.86973541144037370 ) ) ;
#2860=ADVANCED_FACE ( 'NONE', ( #6322 ), #3232, .F. ) ;
#2868=CARTESIAN_POINT ( 'NONE',  ( -63.59366733544099048, -218.0630240738405803, 79.12540989558915783 ) ) ;
#2879=EDGE_LOOP ( 'NONE', ( #6127, #6555, #6819, #5590 ) ) ;
#2880=VERTEX_POINT ( 'NONE', #6650 ) ;
#2908=VERTEX_POINT ( 'NONE', #3848 ) ;
#2924=ADVANCED_FACE ( 'NONE', ( #3269 ), #7305, .F. ) ;
#2930=ORIENTED_EDGE ( 'NONE', *, *, #4051, .F. ) ;
#2934=EDGE_LOOP ( 'NONE', ( #937, #3918, #5908, #998 ) ) ;
#2936=EDGE_CURVE ( 'NONE', #5543, #7540, #3809, .T. ) ;
#2938=CARTESIAN_POINT ( 'NONE',  ( -26.50000000000002487, 16.00000000000012079, -15.99999999999995914 ) ) ;
#2945=EDGE_CURVE ( 'NONE', #2880, #7372, #873, .T. ) ;
#2959=ORIENTED_EDGE ( 'NONE', *, *, #6700, .T. ) ;
#2960=CARTESIAN_POINT ( 'NONE',  ( -60.66255603274095165, -217.0856944719846524, 71.67965750360853860 ) ) ;
#2966=VERTEX_POINT ( 'NONE', #6114 ) ;
#2971=VERTEX_POINT ( 'NONE', #340 ) ;
#2993=AXIS2_PLACEMENT_3D ( 'NONE', #935, #5788, #3364 ) ;
#2995=EDGE_LOOP ( 'NONE', ( #6406, #2420, #5817, #5603 ) ) ;
#2998=VECTOR ( 'NONE', #1613, 1000.000000000000000 ) ;
#3001=CARTESIAN_POINT ( 'NONE',  ( -70.21559789597881718, -217.6453243769069559, 77.74120035865658451 ) ) ;
#3004=DIRECTION ( 'NONE',  ( 1.000000000000000000, 2.465190328815661892E-32, -9.244463733058732095E-33 ) ) ;
#3009=VECTOR ( 'NONE', #4833, 1000.000000000000114 ) ;
#3018=FACE_OUTER_BOUND ( 'NONE', #1236, .T. ) ;
#3032=CYLINDRICAL_SURFACE ( 'NONE', #4851, 8.000000000000007105 ) ;
#3047=CARTESIAN_POINT ( 'NONE',  ( -60.73846410710429211, -222.1285142276679778, 73.03087698472576506 ) ) ;
#3051=AXIS2_PLACEMENT_3D ( 'NONE', #5352, #6965, #3434 ) ;
#3070=LINE ( 'NONE', #1295, #2140 ) ;
#3075=VECTOR ( 'NONE', #3867, 1000.000000000000227 ) ;
#3081=CARTESIAN_POINT ( 'NONE',  ( -60.67236366837565953, -217.7372475398859706, 71.85424062197719763 ) ) ;
#3083=CARTESIAN_POINT ( 'NONE',  ( -61.07266449636613004, -218.0629854895634594, 91.98311311191383766 ) ) ;
#3096=APPLICATION_CONTEXT ( 'automotive_design' ) ;
#3100=EDGE_CURVE ( 'NONE', #3854, #7274, #2112, .T. ) ;
#3106=CARTESIAN_POINT ( 'NONE',  ( -64.26447795140279595, -223.0648723219386511, 82.43246165033174577 ) ) ;
#3107=CARTESIAN_POINT ( 'NONE',  ( -69.37580566599014276, -63.12419433401035462, -8.875805665989638271 ) ) ;
#3110=ORIENTED_EDGE ( 'NONE', *, *, #3842, .F. ) ;
#3113=CARTESIAN_POINT ( 'NONE',  ( -70.03121585365657609, -225.8512969706634408, 79.74927943323393720 ) ) ;
#3115=CARTESIAN_POINT ( 'NONE',  ( -64.50000000000000000, -39.68629150101521219, 16.00000000000001421 ) ) ;
#3116=CARTESIAN_POINT ( 'NONE',  ( -57.62345916743081631, -218.0630240738404950, 94.30959155535899185 ) ) ;
#3118=ORIENTED_EDGE ( 'NONE', *, *, #1053, .T. ) ;
#3144=CARTESIAN_POINT ( 'NONE',  ( -64.51262296323307055, -223.0630240738404098, 85.62222623059837190 ) ) ;
#3148=CARTESIAN_POINT ( 'NONE',  ( -53.06880420804609599, -218.8824061789517259, 72.16108495452195370 ) ) ;
#3150=ADVANCED_FACE ( 'NONE', ( #3961 ), #1068, .F. ) ;
#3155=CARTESIAN_POINT ( 'NONE',  ( -64.47552857335868737, -218.0623681019555420, 84.48708328684777769 ) ) ;
#3166=AXIS2_PLACEMENT_3D ( 'NONE', #2047, #4401, #1462 ) ;
#3172=CARTESIAN_POINT ( 'NONE',  ( -26.50000000000003197, -39.68629150101522640, 24.00000000000002132 ) ) ;
#3177=LINE ( 'NONE', #5525, #4392 ) ;
#3180=CARTESIAN_POINT ( 'NONE',  ( -64.00645916684678127, -223.0646730209604698, 81.35415196545162075 ) ) ;
#3199=ORIENTED_EDGE ( 'NONE', *, *, #5889, .T. ) ;
#3217=CARTESIAN_POINT ( 'NONE',  ( -64.50000000000000000, -49.37258300203048123, -15.99999999999998579 ) ) ;
#3219=CARTESIAN_POINT ( 'NONE',  ( -60.04440983696338918, -223.0634580850465625, 75.61957205288878470 ) ) ;
#3222=AXIS2_PLACEMENT_3D ( 'NONE', #1541, #2124, #2205 ) ;
#3232=( BOUNDED_SURFACE ( )  B_SPLINE_SURFACE ( 5, 3, ( 
 ( #3248, #393, #2817, #7438, #7508, #1618, #469, #6200, #5629, #890, #5021, #2700, #5132, #5053, #2089, #5092 ),
 ( #1466, #1048, #7392, #7355, #353, #4440, #2665, #5599, #6821, #3977, #3408, #4477, #2249, #323, #3906, #6240 ),
 ( #968, #2168, #6280, #1008, #3362, #1845, #6615, #7082, #3698, #6469, #1880, #2460, #1228, #5391, #121, #4816 ),
 ( #6938, #6548, #1922, #3113, #4748, #158, #3624, #7153, #5428, #1811, #5887, #4125, #3001, #4274, #613, #3587 ),
 ( #4165, #6507, #5965, #692, #6040, #5925, #1189, #762, #4237, #3047, #651, #3548, #5356, #3081, #4201, #2960 ),
 ( #2495, #5467, #84, #2425, #1337, #1265, #4783, #7119, #6582, #1304, #198, #7193, #4595, #3665, #5309, #1768 ) ),
 .UNSPECIFIED., .F., .F., .T. ) 
 B_SPLINE_SURFACE_WITH_KNOTS ( ( 6, 6 ),
 ( 4, 2, 2, 2, 2, 2, 2, 4 ),
 ( 0.000000000000000000, 1.000000000000000000 ),
 ( -1.150125124083905659, -0.9546592037126467867, -0.4819498650540673390, 0.000000000000000000, 0.02616758540912784634, 0.5083707369372295615, 0.9999999999999414912, 1.195465920371200363 ),
 .UNSPECIFIED. ) 
 GEOMETRIC_REPRESENTATION_ITEM ( )  RATIONAL_B_SPLINE_SURFACE ( (
 ( 1.000000000000000000, 1.000000000000000000, 1.000000000000000000, 1.000000000000000000, 1.000000000000000000, 1.000000000000000000, 1.000000000000000000, 1.000000000000000000, 1.000000000000000000, 1.000000000000000000, 1.000000000000000000, 1.000000000000000000, 1.000000000000000000, 1.000000000000000000, 1.000000000000000000, 1.000000000000000000),
 ( 0.5999999999999995337, 0.5999999999999995337, 0.5999999999999999778, 0.5999999999999999778, 0.5999999999999999778, 0.5999999999999999778, 0.5999999999999999778, 0.5999999999999999778, 0.5999999999999995337, 0.5999999999999995337, 0.5999999999999999778, 0.5999999999999999778, 0.5999999999999989786, 0.5999999999999989786, 0.5999999999999995337, 0.5999999999999995337),
 ( 0.3999999999999993561, 0.3999999999999993561, 0.4000000000000000777, 0.4000000000000000777, 0.4000000000000000777, 0.4000000000000000777, 0.4000000000000000777, 0.4000000000000000777, 0.3999999999999993561, 0.3999999999999993561, 0.4000000000000000777, 0.4000000000000000777, 0.3999999999999984679, 0.3999999999999984679, 0.3999999999999993561, 0.3999999999999993561),
 ( 0.3999999999999993561, 0.3999999999999993561, 0.4000000000000000777, 0.4000000000000000777, 0.4000000000000000777, 0.4000000000000000777, 0.4000000000000000777, 0.4000000000000000777, 0.3999999999999993561, 0.3999999999999993561, 0.4000000000000000777, 0.4000000000000000777, 0.3999999999999984679, 0.3999999999999984679, 0.3999999999999993561, 0.3999999999999993561),
 ( 0.5999999999999995337, 0.5999999999999995337, 0.5999999999999999778, 0.5999999999999999778, 0.5999999999999999778, 0.5999999999999999778, 0.5999999999999999778, 0.5999999999999999778, 0.5999999999999995337, 0.5999999999999995337, 0.5999999999999999778, 0.5999999999999999778, 0.5999999999999989786, 0.5999999999999989786, 0.5999999999999995337, 0.5999999999999995337),
 ( 1.000000000000000000, 1.000000000000000000, 1.000000000000000000, 1.000000000000000000, 1.000000000000000000, 1.000000000000000000, 1.000000000000000000, 1.000000000000000000, 1.000000000000000000, 1.000000000000000000, 1.000000000000000000, 1.000000000000000000, 1.000000000000000000, 1.000000000000000000, 1.000000000000000000, 1.000000000000000000) ) ) 
 REPRESENTATION_ITEM ( '' )  SURFACE ( )  );
#3247=AXIS2_PLACEMENT_3D ( 'NONE', #1045, #5244, #4089 ) ;
#3248=CARTESIAN_POINT ( 'NONE',  ( -53.51728042240002026, -224.0594585235269847, 96.26692417614293618 ) ) ;
#3253=ORIENTED_EDGE ( 'NONE', *, *, #3541, .F. ) ;
#3260=CARTESIAN_POINT ( 'NONE',  ( -62.90859119154448820, -223.0635329001938771, 78.89259148748521966 ) ) ;
#3269=FACE_OUTER_BOUND ( 'NONE', #2995, .T. ) ;
#3270=ORIENTED_EDGE ( 'NONE', *, *, #5828, .T. ) ;
#3271=EDGE_CURVE ( 'NONE', #7561, #5778, #6539, .T. ) ;
#3280=ORIENTED_EDGE ( 'NONE', *, *, #6968, .T. ) ;
#3284=DIRECTION ( 'NONE',  ( -1.000000000000000000, -1.725633230170963324E-31, 1.078147950931789387E-16 ) ) ;
#3285=CARTESIAN_POINT ( 'NONE',  ( -64.50000000000000000, -218.0630240738404950, 95.20959099461346398 ) ) ;
#3296=CARTESIAN_POINT ( 'NONE',  ( -57.09769269110365997, -223.0630240738405803, 95.49530934758278988 ) ) ;
#3299=CARTESIAN_POINT ( 'NONE',  ( -58.92633973340381459, -218.0624722072869872, 93.67408273893140347 ) ) ;
#3304=CARTESIAN_POINT ( 'NONE',  ( -53.25562355766781053, -223.0194114314942908, 73.26959217102401567 ) ) ;
#3306=DIRECTION ( 'NONE',  ( 1.000000000000000000, 4.437342591868191405E-31, -3.379803290564627601E-16 ) ) ;
#3307=CARTESIAN_POINT ( 'NONE',  ( -26.50000000000003197, -39.68629150101520509, 16.00000000000001421 ) ) ;
#3308=ORIENTED_EDGE ( 'NONE', *, *, #2042, .T. ) ;
#3316=EDGE_LOOP ( 'NONE', ( #1488, #5210, #1332, #4974, #509 ) ) ;
#3323=CARTESIAN_POINT ( 'NONE',  ( -64.50000000000000000, -39.68629150101522640, 16.00000000000001421 ) ) ;
#3334=DIRECTION ( 'NONE',  ( 1.000000000000000000, 2.465190328815661892E-32, -9.244463733058732095E-33 ) ) ;
#3336=DIRECTION ( 'NONE',  ( -2.465190328815661892E-32, -0.7071067811865465735, 0.7071067811865484609 ) ) ;
#3339=CARTESIAN_POINT ( 'NONE',  ( -57.47262553190106615, -218.0630247163618094, 72.86387756518055880 ) ) ;
#3340=VERTEX_POINT ( 'NONE', #186 ) ;
#3343=DIRECTION ( 'NONE',  ( -2.465190328815661892E-32, -1.000000000000000000, -1.193489751472043281E-15 ) ) ;
#3349=EDGE_CURVE ( 'NONE', #920, #3850, #2101, .T. ) ;
#3350=PRODUCT_DEFINITION ( 'UNKNOWN', '', #7315, #1175 ) ;
#3352=ORIENTED_EDGE ( 'NONE', *, *, #4544, .F. ) ;
#3362=CARTESIAN_POINT ( 'NONE',  ( -70.04900473833201602, -222.6575489669631054, 90.39048551345001670 ) ) ;
#3364=DIRECTION ( 'NONE',  ( 9.244463733058733463E-33, 0.000000000000000000, -1.000000000000000000 ) ) ;
#3368=EDGE_CURVE ( 'NONE', #5318, #2966, #3690, .T. ) ;
#3371=VECTOR ( 'NONE', #1802, 1000.000000000000000 ) ;
#3378=CIRCLE ( 'NONE', #5472, 15.99999999999998934 ) ;
#3381=ORIENTED_EDGE ( 'NONE', *, *, #3822, .F. ) ;
#3396=DIRECTION ( 'NONE',  ( 0.000000000000000000, 0.000000000000000000, -1.000000000000000000 ) ) ;
#3404=FACE_OUTER_BOUND ( 'NONE', #2017, .T. ) ;
#3408=CARTESIAN_POINT ( 'NONE',  ( -60.72636667137881261, -216.4242598635585182, 94.92063264932016864 ) ) ;
#3410=LINE ( 'NONE', #3941, #6179 ) ;
#3411=AXIS2_PLACEMENT_3D ( 'NONE', #145, #6026, #749 ) ;
#3412=VERTEX_POINT ( 'NONE', #7221 ) ;
#3414=ORIENTED_EDGE ( 'NONE', *, *, #5977, .F. ) ;
#3423=CARTESIAN_POINT ( 'NONE',  ( -58.07354361304951595, -218.0631760585727932, 73.14332378351642205 ) ) ;
#3434=DIRECTION ( 'NONE',  ( 4.336808689942025132E-16, 2.255140518769853009E-14, 1.000000000000000000 ) ) ;
#3441=DIRECTION ( 'NONE',  ( -1.000000000000000000, -1.725633230170963324E-31, 1.078147950931789387E-16 ) ) ;
#3445=CARTESIAN_POINT ( 'NONE',  ( -26.52830334398518985, -116.3958977277557807, 43.92260702357706492 ) ) ;
#3458=CARTESIAN_POINT ( 'NONE',  ( -63.83888562197329009, -218.0637078869157506, 79.76758675555454658 ) ) ;
#3464=CARTESIAN_POINT ( 'NONE',  ( -26.50000000000003197, -49.37258300203047412, 0.000000000000000000 ) ) ;
#3467=DIRECTION ( 'NONE',  ( 1.000000000000000000, 2.465190328815661892E-32, -9.244463733058732095E-33 ) ) ;
#3477=VERTEX_POINT ( 'NONE', #1095 ) ;
#3488=CARTESIAN_POINT ( 'NONE',  ( -26.50000000000003197, -102.6862915010150346, 30.68629150101517666 ) ) ;
#3490=UNCERTAINTY_MEASURE_WITH_UNIT (LENGTH_MEASURE( 1.000000000000000082E-05 ), #743, 'distance_accuracy_value', 'NONE');
#3497=LINE ( 'NONE', #4192, #4354 ) ;
#3498=DIRECTION ( 'NONE',  ( 1.000000000000000000, 2.465190328815661892E-32, -9.244463733058732095E-33 ) ) ;
#3503=VERTEX_POINT ( 'NONE', #2180 ) ;
#3506=CARTESIAN_POINT ( 'NONE',  ( -26.50000000000003197, 0.000000000000000000, 0.000000000000000000 ) ) ;
#3507=CARTESIAN_POINT ( 'NONE',  ( -29.64230087749236731, -65.39789427971169289, 38.39789427971179947 ) ) ;
#3516=ORIENTED_EDGE ( 'NONE', *, *, #5438, .T. ) ;
#3517=LINE ( 'NONE', #432, #2998 ) ;
#3529=CARTESIAN_POINT ( 'NONE',  ( -64.50000000000000000, -99.90626354475342907, 72.90626354475362803 ) ) ;
#3533=EDGE_LOOP ( 'NONE', ( #7260, #6874, #5584, #3627, #3308, #3765, #1999 ) ) ;
#3541=EDGE_CURVE ( 'NONE', #3477, #2174, #980, .T. ) ;
#3544=EDGE_CURVE ( 'NONE', #4795, #3854, #480, .T. ) ;
#3545=FACE_BOUND ( 'NONE', #2274, .T. ) ;
#3546=CARTESIAN_POINT ( 'NONE',  ( -53.47314606205194565, -223.0630240738404950, 96.09122589815579829 ) ) ;
#3548=CARTESIAN_POINT ( 'NONE',  ( -60.70193531918452123, -219.7017882839737695, 72.38063772785841365 ) ) ;
#3568=STYLED_ITEM('',(#7631),#3747);
#3569=PLANE ( 'NONE',  #1929 ) ;
#3578=( BOUNDED_CURVE ( )  B_SPLINE_CURVE ( 3, ( #6657, #1379, #3742, #6083 ),
 .UNSPECIFIED., .F., .T. ) 
 B_SPLINE_CURVE_WITH_KNOTS ( ( 4, 4 ),
 ( 0.7853981633974504994, 1.570796326794896558 ),
 .UNSPECIFIED. ) 
 CURVE ( )  GEOMETRIC_REPRESENTATION_ITEM ( )  RATIONAL_B_SPLINE_CURVE ( ( 1.000000000000000000, 0.9492530216741914550, 0.9492530216741914550, 1.000000000000000000 ) ) 
 REPRESENTATION_ITEM ( '' )  );
#3587=CARTESIAN_POINT ( 'NONE',  ( -70.25616595088855831, -215.8398321358105818, 77.29937933778069237 ) ) ;
#3596=ORIENTED_EDGE ( 'NONE', *, *, #2800, .F. ) ;
#3600=ORIENTED_EDGE ( 'NONE', *, *, #1954, .T. ) ;
#3624=CARTESIAN_POINT ( 'NONE',  ( -70.10306686690893230, -222.6535482193572477, 78.96676008164921257 ) ) ;
#3626=CARTESIAN_POINT ( 'NONE',  ( -64.50000000000000000, 0.000000000000000000, 15.99999999999998579 ) ) ;
#3627=ORIENTED_EDGE ( 'NONE', *, *, #6450, .T. ) ;
#3634=DIRECTION ( 'NONE',  ( 1.000000000000000000, 2.465190328815661892E-32, -9.244463733058732095E-33 ) ) ;
#3659=ORIENTED_EDGE ( 'NONE', *, *, #5209, .F. ) ;
#3665=CARTESIAN_POINT ( 'NONE',  ( -53.01709100512437089, -217.7372475398855443, 71.85424062197864714 ) ) ;
#3666=DIRECTION ( 'NONE',  ( 3.379803290564627601E-16, -1.193489751472043281E-15, 1.000000000000000000 ) ) ;
#3667=CARTESIAN_POINT ( 'NONE',  ( -63.70446932513453220, -218.0630240022875910, 87.95745700536116374 ) ) ;
#3675=DIRECTION ( 'NONE',  ( -2.465190328815661892E-32, -1.000000000000000000, -1.193489751472043281E-15 ) ) ;
#3681=EDGE_CURVE ( 'NONE', #589, #2111, #5837, .T. ) ;
#3688=LINE ( 'NONE', #3217, #5597 ) ;
#3690=LINE ( 'NONE', #3803, #6883 ) ;
#3693=EDGE_LOOP ( 'NONE', ( #2041, #7579, #6400, #1850 ) ) ;
#3694=DIRECTION ( 'NONE',  ( 9.244463733058733463E-33, 0.000000000000000000, -1.000000000000000000 ) ) ;
#3696=VECTOR ( 'NONE', #7518, 1000.000000000000000 ) ;
#3698=CARTESIAN_POINT ( 'NONE',  ( -70.12317295347672541, -219.3245666396718718, 89.72755010419726318 ) ) ;
#3700=CARTESIAN_POINT ( 'NONE',  ( -64.49624945276272570, -218.0628238658616738, 84.01119032334271708 ) ) ;
#3705=PLANE ( 'NONE',  #7184 ) ;
#3727=CARTESIAN_POINT ( 'NONE',  ( -57.41291415210449856, -223.0630401650004728, 74.10192998188830416 ) ) ;
#3732=ORIENTED_EDGE ( 'NONE', *, *, #5945, .T. ) ;
#3736=CARTESIAN_POINT ( 'NONE',  ( -63.29904432569978212, -218.0627255230571677, 88.88647797590476785 ) ) ;
#3737=EDGE_LOOP ( 'NONE', ( #4821, #1293, #696, #5057 ) ) ;
#3742=CARTESIAN_POINT ( 'NONE',  ( -26.50000000000002487, -104.8363803175325444, 32.83638031753270070 ) ) ;
#3747=MANIFOLD_SOLID_BREP ( '<left arm>-<Fillet3>', #6265 ) ;
#3748=CARTESIAN_POINT ( 'NONE',  ( -24.15685424949240101, 16.00000000000007105, 36.34314575050770202 ) ) ;
#3751=CIRCLE ( 'NONE', #1399, 6.000000000000000000 ) ;
#3764=CARTESIAN_POINT ( 'NONE',  ( -57.47793317182449613, -223.0630299184109333, 74.12895951337506517 ) ) ;
#3765=ORIENTED_EDGE ( 'NONE', *, *, #6176, .T. ) ;
#3768=ORIENTED_EDGE ( 'NONE', *, *, #3271, .F. ) ;
#3773=AXIS2_PLACEMENT_3D ( 'NONE', #4262, #5948, #679 ) ;
#3774=B_SPLINE_CURVE_WITH_KNOTS ( 'NONE', 3,
 ( #347, #1571, #5046, #2772 ),
 .UNSPECIFIED., .F., .F.,
 ( 4, 4 ),
 ( 3.469446951953635759E-17, 0.0007743866022177889373 ),
 .UNSPECIFIED. ) ;
#3777=ORIENTED_EDGE ( 'NONE', *, *, #1072, .F. ) ;
#3779=( BOUNDED_CURVE ( )  B_SPLINE_CURVE ( 3, ( #6549, #4276, #5926, #7040 ),
 .UNSPECIFIED., .F., .T. ) 
 B_SPLINE_CURVE_WITH_KNOTS ( ( 4, 4 ),
 ( 3.926990816987244060, 4.712388980384692339 ),
 .UNSPECIFIED. ) 
 CURVE ( )  GEOMETRIC_REPRESENTATION_ITEM ( )  RATIONAL_B_SPLINE_CURVE ( ( 1.000000000000000000, 0.9492530216741911220, 0.9492530216741911220, 1.000000000000000000 ) ) 
 REPRESENTATION_ITEM ( '' )  );
#3783=DIRECTION ( 'NONE',  ( 0.7660444431189621373, 1.387778780781445676E-17, 0.6427876096865583477 ) ) ;
#3784=CARTESIAN_POINT ( 'NONE',  ( -29.64230087749237086, -110.3978942797115650, 38.39789427971174263 ) ) ;
#3801=CARTESIAN_POINT ( 'NONE',  ( -57.12880255235567972, -223.0631510105118309, 73.98989896671450595 ) ) ;
#3803=CARTESIAN_POINT ( 'NONE',  ( -64.50000000000000000, -7.347880794884119736E-16, -6.000000000000000000 ) ) ;
#3806=ADVANCED_FACE ( 'NONE', ( #4330 ), #5488, .F. ) ;
#3809=LINE ( 'NONE', #6178, #512 ) ;
#3810=ORIENTED_EDGE ( 'NONE', *, *, #6700, .F. ) ;
#3822=EDGE_CURVE ( 'NONE', #7561, #2908, #2074, .T. ) ;
#3825=DIRECTION ( 'NONE',  ( 1.000000000000000000, 2.465190328815661892E-32, -9.244463733058732095E-33 ) ) ;
#3839=CARTESIAN_POINT ( 'NONE',  ( -58.82507573250082089, -223.0635350528836511, 74.77305146519802292 ) ) ;
#3842=EDGE_CURVE ( 'NONE', #5048, #917, #970, .T. ) ;
#3848=CARTESIAN_POINT ( 'NONE',  ( -26.50000000000000711, -117.9145199278634806, 44.76505905230362714 ) ) ;
#3850=VERTEX_POINT ( 'NONE', #7394 ) ;
#3854=VERTEX_POINT ( 'NONE', #4442 ) ;
#3867=DIRECTION ( 'NONE',  ( 0.5773502691896309491, -0.5773502691896224004, 0.5773502691896238437 ) ) ;
#3868=EDGE_CURVE ( 'NONE', #5394, #2971, #3410, .T. ) ;
#3876=CARTESIAN_POINT ( 'NONE',  ( -60.25732134435390464, -223.0624617060423986, 93.74339436655736790 ) ) ;
#3879=VECTOR ( 'NONE', #2617, 1000.000000000000000 ) ;
#3881=CARTESIAN_POINT ( 'NONE',  ( -61.77318701999629980, -218.0630240738405234, 91.25301986902242390 ) ) ;
#3883=ORIENTED_EDGE ( 'NONE', *, *, #7005, .T. ) ;
#3884=EDGE_CURVE ( 'NONE', #5471, #312, #7496, .T. ) ;
#3886=CARTESIAN_POINT ( 'NONE',  ( -53.21539232130207608, -222.1285142276788065, 73.03087698472252498 ) ) ;
#3889=CARTESIAN_POINT ( 'NONE',  ( -64.50000000000000000, -6.938893903907228378E-15, -15.99999999999998579 ) ) ;
#3896=PLANE ( 'NONE',  #7501 ) ;
#3897=CARTESIAN_POINT ( 'NONE',  ( -18.49999999999999289, 16.00000000000007105, 30.68629150101529035 ) ) ;
#3900=ADVANCED_FACE ( 'NONE', ( #1010 ), #5171, .F. ) ;
#3906=CARTESIAN_POINT ( 'NONE',  ( -60.66745985056437007, -212.4343899438517269, 94.21711093295449757 ) ) ;
#3908=CARTESIAN_POINT ( 'NONE',  ( -21.49999999999999289, 16.00000000000004263, 42.31370849898488729 ) ) ;
#3914=FACE_OUTER_BOUND ( 'NONE', #2934, .T. ) ;
#3918=ORIENTED_EDGE ( 'NONE', *, *, #4663, .F. ) ;
#3935=LINE ( 'NONE', #3285, #7304 ) ;
#3941=CARTESIAN_POINT ( 'NONE',  ( -64.50000000000000000, -6.938893903907228378E-15, -15.99999999999998579 ) ) ;
#3951=DIRECTION ( 'NONE',  ( 1.000000000000000000, 2.465190328815661892E-32, -9.244463733058732095E-33 ) ) ;
#3953=CARTESIAN_POINT ( 'NONE',  ( -60.56776133228527925, -218.0630240738405234, 74.80990615958565115 ) ) ;
#3954=EDGE_CURVE ( 'NONE', #3477, #228, #2170, .T. ) ;
#3958=CARTESIAN_POINT ( 'NONE',  ( -29.35769912250765046, 16.00000000000004263, 38.63670350735201708 ) ) ;
#3961=FACE_OUTER_BOUND ( 'NONE', #4627, .T. ) ;
#3977=CARTESIAN_POINT ( 'NONE',  ( -60.73846410710429211, -217.2436419687046509, 95.06511182196476284 ) ) ;
#3979=CARTESIAN_POINT ( 'NONE',  ( -26.50000000000000711, -117.9145199278634806, 44.76505905230362714 ) ) ;
#3988=CARTESIAN_POINT ( 'NONE',  ( -53.47314606205194565, -223.0630240738404950, 96.09122589815579829 ) ) ;
#3991=CARTESIAN_POINT ( 'NONE',  ( -63.63476818105571908, -218.0630489433316370, 79.22587972011848478 ) ) ;
#3994=VERTEX_POINT ( 'NONE', #7587 ) ;
#4007=DIRECTION ( 'NONE',  ( 0.000000000000000000, 0.000000000000000000, -1.000000000000000000 ) ) ;
#4015=ORIENTED_EDGE ( 'NONE', *, *, #6333, .F. ) ;
#4016=ORIENTED_EDGE ( 'NONE', *, *, #3349, .T. ) ;
#4017=VECTOR ( 'NONE', #2568, 1000.000000000000000 ) ;
#4018=DIRECTION ( 'NONE',  ( -2.465190328815661892E-32, -1.000000000000000000, -1.193489751472043281E-15 ) ) ;
#4031=CARTESIAN_POINT ( 'NONE',  ( -61.43119716943146358, -223.0630215652982713, 92.62836485985936008 ) ) ;
#4034=CARTESIAN_POINT ( 'NONE',  ( -62.03747301282925974, -218.0635026243406287, 76.42168781368546604 ) ) ;
#4041=FACE_OUTER_BOUND ( 'NONE', #3533, .T. ) ;
#4048=CARTESIAN_POINT ( 'NONE',  ( -26.50000000000000711, -71.76505905230354188, 44.76505905230365556 ) ) ;
#4051=EDGE_CURVE ( 'NONE', #7274, #3854, #6061, .T. ) ;
#4058=DIRECTION ( 'NONE',  ( -9.860761315262649757E-32, 1.000000000000000000, 0.000000000000000000 ) ) ;
#4061=ADVANCED_FACE ( 'NONE', ( #3018 ), #4717, .F. ) ;
#4068=CARTESIAN_POINT ( 'NONE',  ( -64.50000000000000000, -45.34314575050760254, 18.34314575050763452 ) ) ;
#4070=ORIENTED_EDGE ( 'NONE', *, *, #4334, .F. ) ;
#4080=VERTEX_POINT ( 'NONE', #627 ) ;
#4082=EDGE_CURVE ( 'NONE', #4118, #1397, #4641, .T. ) ;
#4086=LINE ( 'NONE', #4785, #192 ) ;
#4089=DIRECTION ( 'NONE',  ( 0.000000000000000000, 0.000000000000000000, 1.000000000000000000 ) ) ;
#4118=VERTEX_POINT ( 'NONE', #7094 ) ;
#4120=VECTOR ( 'NONE', #1863, 1000.000000000000000 ) ;
#4122=LINE ( 'NONE', #2380, #4769 ) ;
#4125=CARTESIAN_POINT ( 'NONE',  ( -70.19709702122540307, -218.4687108041560180, 77.94269080187309839 ) ) ;
#4130=ORIENTED_EDGE ( 'NONE', *, *, #561, .F. ) ;
#4140=CARTESIAN_POINT ( 'NONE',  ( -26.50000000000000355, -120.9522879036833558, 45.92078884797940219 ) ) ;
#4144=CARTESIAN_POINT ( 'NONE',  ( -27.07790214619733860, -113.7796841263389069, 41.77968412633906325 ) ) ;
#4153=DIRECTION ( 'NONE',  ( -3.081487911019577365E-33, -1.193489751472043281E-15, 1.000000000000000000 ) ) ;
#4161=ORIENTED_EDGE ( 'NONE', *, *, #4082, .T. ) ;
#4165=CARTESIAN_POINT ( 'NONE',  ( -60.83909347413334245, -228.8136496942593112, 74.82215363428544208 ) ) ;
#4173=SHAPE_DEFINITION_REPRESENTATION ( #7078, #7252 ) ;
#4192=CARTESIAN_POINT ( 'NONE',  ( -23.84314575050761320, 16.00000000000004619, 36.65685424949246851 ) ) ;
#4199=DIRECTION ( 'NONE',  ( 1.000000000000000000, 2.465190328815661892E-32, -9.244463733058732095E-33 ) ) ;
#4201=CARTESIAN_POINT ( 'NONE',  ( -60.66745985056476798, -217.4114710059388926, 71.76694906279429631 ) ) ;
#4204=CARTESIAN_POINT ( 'NONE',  ( -62.83175576870043955, -218.0623705734561497, 89.75267118170498293 ) ) ;
#4212=DIRECTION ( 'NONE',  ( 0.000000000000000000, 0.000000000000000000, -1.000000000000000000 ) ) ;
#4230=ORIENTED_EDGE ( 'NONE', *, *, #5643, .F. ) ;
#4232=EDGE_CURVE ( 'NONE', #5048, #3850, #1383, .T. ) ;
#4233=DIRECTION ( 'NONE',  ( -1.000000000000000000, -2.465190328815661892E-32, -9.244463733058733463E-33 ) ) ;
#4234=VECTOR ( 'NONE', #3825, 1000.000000000000000 ) ;
#4235=CARTESIAN_POINT ( 'NONE',  ( -53.25562355766777500, -218.1519544391844079, 95.22527181742783853 ) ) ;
#4237=CARTESIAN_POINT ( 'NONE',  ( -60.75121803101544060, -222.9757987891385369, 73.25790619872466891 ) ) ;
#4239=CARTESIAN_POINT ( 'NONE',  ( -54.71793473364260052, -218.0620782339077834, 95.13813623280537968 ) ) ;
#4253=CARTESIAN_POINT ( 'NONE',  ( -32.50000000000001421, -106.6736682753135739, 34.67366827531368756 ) ) ;
#4256=CARTESIAN_POINT ( 'NONE',  ( -29.50000000000000000, -223.0630240738404950, 73.28127814332044920 ) ) ;
#4257=ORIENTED_EDGE ( 'NONE', *, *, #4624, .T. ) ;
#4262=CARTESIAN_POINT ( 'NONE',  ( -26.50000000000003197, 0.000000000000000000, 0.000000000000000000 ) ) ;
#4265=CARTESIAN_POINT ( 'NONE',  ( -60.94741519416551512, -223.0630598631611861, 76.40853535907753269 ) ) ;
#4270=ORIENTED_EDGE ( 'NONE', *, *, #4361, .F. ) ;
#4274=CARTESIAN_POINT ( 'NONE',  ( -70.24145449743711822, -216.4945693450226543, 77.45959972289216466 ) ) ;
#4275=EDGE_CURVE ( 'NONE', #1071, #5437, #421, .T. ) ;
#4276=CARTESIAN_POINT ( 'NONE',  ( -22.32280336819470890, -65.17719663180518808, 38.17719663180528045 ) ) ;
#4277=CARTESIAN_POINT ( 'NONE',  ( -64.38803740020385646, -218.0613621616423927, 85.37521886293086482 ) ) ;
#4282=VERTEX_POINT ( 'NONE', #6012 ) ;
#4285=ADVANCED_FACE ( 'NONE', ( #7164 ), #6593, .F. ) ;
#4292=CARTESIAN_POINT ( 'NONE',  ( -32.50000000000001421, -99.90626354475344328, 72.90626354475362803 ) ) ;
#4300=CARTESIAN_POINT ( 'NONE',  ( -63.74607179430710602, -223.0630176522924444, 88.91434613420386768 ) ) ;
#4304=ORIENTED_EDGE ( 'NONE', *, *, #1053, .F. ) ;
#4307=CARTESIAN_POINT ( 'NONE',  ( -22.45815546247371586, -110.0418445375260603, 38.04184453752623796 ) ) ;
#4311=CARTESIAN_POINT ( 'NONE',  ( -61.28154286849950694, -218.0630231266628698, 91.76994857279252926 ) ) ;
#4329=LINE ( 'NONE', #1393, #4808 ) ;
#4330=FACE_OUTER_BOUND ( 'NONE', #1193, .T. ) ;
#4334=EDGE_CURVE ( 'NONE', #228, #5778, #3774, .T. ) ;
#4338=CARTESIAN_POINT ( 'NONE',  ( -63.80434472310041372, -223.0629276316900018, 88.75851834311229993 ) ) ;
#4354=VECTOR ( 'NONE', #5267, 1000.000000000000000 ) ;
#4358=FACE_OUTER_BOUND ( 'NONE', #534, .T. ) ;
#4361=EDGE_CURVE ( 'NONE', #2111, #3994, #4549, .T. ) ;
#4364=( BOUNDED_CURVE ( )  B_SPLINE_CURVE ( 3, ( #6219, #2834, #5034, #6875 ),
 .UNSPECIFIED., .F., .T. ) 
 B_SPLINE_CURVE_WITH_KNOTS ( ( 4, 4 ),
 ( 1.570796326794896558, 3.141592653589793116 ),
 .UNSPECIFIED. ) 
 CURVE ( )  GEOMETRIC_REPRESENTATION_ITEM ( )  RATIONAL_B_SPLINE_CURVE ( ( 1.000000000000000000, 0.8047378541243649375, 0.8047378541243649375, 1.000000000000000000 ) ) 
 REPRESENTATION_ITEM ( '' )  );
#4373=CARTESIAN_POINT ( 'NONE',  ( -29.35769912250765046, -110.6367035073516831, 38.63670350735182524 ) ) ;
#4379=DIRECTION ( 'NONE',  ( 1.000000000000000000, 2.465190328815661892E-32, -9.244463733058732095E-33 ) ) ;
#4382=CARTESIAN_POINT ( 'NONE',  ( -61.12936385255436988, -223.0630265135370109, 76.58851298612765390 ) ) ;
#4389=DIRECTION ( 'NONE',  ( -2.465190328815661892E-32, -1.000000000000000000, -1.193489751472043281E-15 ) ) ;
#4392=VECTOR ( 'NONE', #4379, 1000.000000000000000 ) ;
#4393=ORIENTED_EDGE ( 'NONE', *, *, #3368, .T. ) ;
#4395=CIRCLE ( 'NONE', #3166, 6.000000000000000888 ) ;
#4401=DIRECTION ( 'NONE',  ( -1.000000000000000000, -1.725633230170963324E-31, 1.078147950931789387E-16 ) ) ;
#4402=ADVANCED_FACE ( 'NONE', ( #1493 ), #1535, .F. ) ;
#4420=DIRECTION ( 'NONE',  ( 6.162975822039156098E-33, 0.2588190451025209060, 0.9659258262890683122 ) ) ;
#4423=VECTOR ( 'NONE', #3336, 1000.000000000000000 ) ;
#4426=AXIS2_PLACEMENT_3D ( 'NONE', #402, #2748, #7446 ) ;
#4436=DIRECTION ( 'NONE',  ( -2.465190328815661892E-32, -1.000000000000000000, -1.193489751472043281E-15 ) ) ;
#4437=FACE_OUTER_BOUND ( 'NONE', #1659, .T. ) ;
#4440=CARTESIAN_POINT ( 'NONE',  ( -60.77671317003687790, -219.8343230396697834, 95.52191879319202883 ) ) ;
#4442=CARTESIAN_POINT ( 'NONE',  ( -26.50000000000003197, -49.37258300203047412, -6.000000000000002665 ) ) ;
#4448=CARTESIAN_POINT ( 'NONE',  ( -54.91295168136564797, -223.0620909472820586, 96.02094539123626760 ) ) ;
#4450=DIRECTION ( 'NONE',  ( -0.5773502691896309491, 0.5773502691896222894, -0.5773502691896239547 ) ) ;
#4456=CARTESIAN_POINT ( 'NONE',  ( -32.50000000000002842, 6.938893903907228378E-15, 6.000000000000000000 ) ) ;
#4461=EDGE_CURVE ( 'NONE', #5858, #3340, #4086, .T. ) ;
#4468=ORIENTED_EDGE ( 'NONE', *, *, #3541, .T. ) ;
#4476=VECTOR ( 'NONE', #1156, 1000.000000000000000 ) ;
#4477=CARTESIAN_POINT ( 'NONE',  ( -60.70193531918451413, -214.7694783647499719, 94.62885002390540023 ) ) ;
#4482=ORIENTED_EDGE ( 'NONE', *, *, #1352, .F. ) ;
#4490=DIRECTION ( 'NONE',  ( 0.000000000000000000, 0.000000000000000000, 1.000000000000000000 ) ) ;
#4495=CARTESIAN_POINT ( 'NONE',  ( -61.14025695922334336, -218.0630242524650271, 75.39509193528782305 ) ) ;
#4517=VERTEX_POINT ( 'NONE', #4708 ) ;
#4524=CARTESIAN_POINT ( 'NONE',  ( -32.50000000000002132, -59.26953873475993362, 32.26953873476001888 ) ) ;
#4531=CARTESIAN_POINT ( 'NONE',  ( -61.93488458595647472, -223.0627659977873236, 92.05494445931830683 ) ) ;
#4535=CARTESIAN_POINT ( 'NONE',  ( -56.72730684359804343, -218.0630240738404950, 72.54495759198080407 ) ) ;
#4542=DIRECTION ( 'NONE',  ( 1.000000000000000000, 2.465190328815661892E-32, -9.244463733058732095E-33 ) ) ;
#4544=EDGE_CURVE ( 'NONE', #1843, #1754, #5856, .T. ) ;
#4549=LINE ( 'NONE', #386, #6442 ) ;
#4563=( BOUNDED_CURVE ( )  B_SPLINE_CURVE ( 3, ( #1600, #6877, #7489, #5731 ),
 .UNSPECIFIED., .F., .T. ) 
 B_SPLINE_CURVE_WITH_KNOTS ( ( 4, 4 ),
 ( 4.712388980384687898, 5.497787143782134400 ),
 .UNSPECIFIED. ) 
 CURVE ( )  GEOMETRIC_REPRESENTATION_ITEM ( )  RATIONAL_B_SPLINE_CURVE ( ( 1.000000000000000000, 0.9492530216741912330, 0.9492530216741912330, 1.000000000000000000 ) ) 
 REPRESENTATION_ITEM ( '' )  );
#4567=CARTESIAN_POINT ( 'NONE',  ( -58.56925906381054148, -223.0627927779807749, 94.82172945580802548 ) ) ;
#4569=CARTESIAN_POINT ( 'NONE',  ( -64.50000000000000000, -49.37258300203047412, -6.000000000000000888 ) ) ;
#4571=CARTESIAN_POINT ( 'NONE',  ( -62.25657246635859821, -218.0636273854565275, 76.71444954786895210 ) ) ;
#4594=EDGE_CURVE ( 'NONE', #1397, #2880, #1695, .T. ) ;
#4595=CARTESIAN_POINT ( 'NONE',  ( -53.06880420804609599, -218.8824061789517259, 72.16108495452192528 ) ) ;
#4596=CARTESIAN_POINT ( 'NONE',  ( -28.15685424949236548, -218.0630240738404666, 95.20959099461347819 ) ) ;
#4603=CARTESIAN_POINT ( 'NONE',  ( -32.50000000000002842, -49.37258300203047412, 0.000000000000000000 ) ) ;
#4605=CARTESIAN_POINT ( 'NONE',  ( -63.06750362476648775, -223.0623716789916102, 90.42757439449754031 ) ) ;
#4606=DIRECTION ( 'NONE',  ( 0.000000000000000000, 0.000000000000000000, 1.000000000000000000 ) ) ;
#4608=EDGE_CURVE ( 'NONE', #3994, #208, #7268, .T. ) ;
#4609=CARTESIAN_POINT ( 'NONE',  ( -63.61353958389151586, -218.0630304217399669, 79.17370859764169211 ) ) ;
#4613=( BOUNDED_CURVE ( )  B_SPLINE_CURVE ( 3, ( #2844, #5194, #7531, #572 ),
 .UNSPECIFIED., .F., .T. ) 
 B_SPLINE_CURVE_WITH_KNOTS ( ( 4, 4 ),
 ( 4.712388980384690562, 6.283185307179586232 ),
 .UNSPECIFIED. ) 
 CURVE ( )  GEOMETRIC_REPRESENTATION_ITEM ( )  RATIONAL_B_SPLINE_CURVE ( ( 1.000000000000000000, 0.8047378541243652705, 0.8047378541243652705, 1.000000000000000000 ) ) 
 REPRESENTATION_ITEM ( '' )  );
#4620=VECTOR ( 'NONE', #3004, 1000.000000000000000 ) ;
#4624=EDGE_CURVE ( 'NONE', #1413, #7513, #4705, .T. ) ;
#4627=EDGE_LOOP ( 'NONE', ( #5625, #6055, #5336, #6699 ) ) ;
#4633=EDGE_LOOP ( 'NONE', ( #1989, #3600, #6619, #6468 ) ) ;
#4634=VERTEX_POINT ( 'NONE', #5112 ) ;
#4641=LINE ( 'NONE', #6979, #1504 ) ;
#4643=VERTEX_POINT ( 'NONE', #6252 ) ;
#4663=EDGE_CURVE ( 'NONE', #1397, #5394, #1640, .T. ) ;
#4664=FACE_BOUND ( 'NONE', #2142, .T. ) ;
#4666=VERTEX_POINT ( 'NONE', #7352 ) ;
#4671=ADVANCED_FACE ( 'NONE', ( #716 ), #5554, .T. ) ;
#4688=EDGE_CURVE ( 'NONE', #3412, #6889, #2048, .T. ) ;
#4689=EDGE_CURVE ( 'NONE', #7339, #3503, #3070, .T. ) ;
#4699=ORIENTED_EDGE ( 'NONE', *, *, #6155, .F. ) ;
#4705=B_SPLINE_CURVE_WITH_KNOTS ( 'NONE', 3,
 ( #4893, #232, #4239, #695, #1267, #5430, #1419, #5393, #947, #5967, #123, #160, #3116, #5470, #3299, #6004, #2462, #368, #2542, #200, #3083, #1375, #4818, #4311, #6652, #4929, #3881, #2573, #4204, #2713, #3736, #6617, #7156, #7120, #6584, #1996, #1847, #1308, #3667, #4856, #6078, #7195, #805, #1925, #4277, #1339, #3155, #5506, #3700, #1591, #2260, #1096, #5145, #7520, #7403, #3458, #2793, #6871, #5799, #3991, #4609, #450, #520, #7484, #2750, #2868, #5762, #2221, #4571, #4034, #1060, #7448, #6909, #5220, #2831, #2181, #6341, #4495, #981, #3953, #5184, #1630, #6953, #7560, #3423, #6379, #2138, #1020, #481, #3339, #5065, #4535, #6834, #1677, #6294, #1556 ),
 .UNSPECIFIED., .F., .F.,
 ( 4, 2, 2, 2, 1, 1, 2, 2, 2, 2, 2, 1, 1, 1, 2, 2, 2, 2, 2, 1, 1, 1, 1, 1, 2, 2, 2, 2, 2, 2, 2, 2, 2, 2, 1, 1, 1, 1, 1, 2, 2, 2, 2, 2, 1, 1, 1, 2, 2, 2, 2, 2, 1, 1, 2, 2, 2, 4 ),
 ( 0.000000000000000000, 0.06250000000003484713, 0.09375000000005226375, 0.1093750000000608125, 0.1171875000000650868, 0.1210937500000670158, 0.1230468750000682093, 0.1250000000000693889, 0.1875000000000952849, 0.2187500000001082467, 0.2343750000001147138, 0.2421875000001181555, 0.2460937500001195155, 0.2480468750001201816, 0.2490234375001202927, 0.2500000000001204037, 0.3125000000001556533, 0.3437500000001734168, 0.3593750000001822986, 0.3671875000001867395, 0.3710937500001889600, 0.3730468750001900702, 0.3740234375001909028, 0.3745117187501913469, 0.3747558593751918465, 0.3750000000001923461, 0.4375000000002062239, 0.4687500000002127187, 0.4843750000002159384, 0.4921875000002171041, 0.5000000000002181588, 0.5625000000002263745, 0.5937500000002299272, 0.6093750000002309264, 0.6171875000002320366, 0.6210937500002324807, 0.6230468750002324807, 0.6240234375002313705, 0.6245117187502307043, 0.6247558593752309264, 0.6250000000002310374, 0.6875000000002089440, 0.7187500000001981748, 0.7343750000001931788, 0.7421875000001901812, 0.7460937500001887379, 0.7480468750001882938, 0.7490234375001878497, 0.7500000000001872946, 0.8125000000001266764, 0.8437500000000963674, 0.8593750000000810463, 0.8671875000000730527, 0.8710937500000696110, 0.8730468750000682787, 0.8750000000000670575, 0.9375000000000335287, 1.000000000000000000 ),
 .UNSPECIFIED. ) ;
#4706=ADVANCED_FACE ( 'NONE', ( #5049 ), #929, .F. ) ;
#4708=CARTESIAN_POINT ( 'NONE',  ( -29.35769912250765046, -65.63670350735181103, 38.63670350735190340 ) ) ;
#4715=EDGE_LOOP ( 'NONE', ( #605, #1697, #2102, #3280 ) ) ;
#4717=PLANE ( 'NONE',  #2000 ) ;
#4746=FACE_OUTER_BOUND ( 'NONE', #4715, .T. ) ;
#4748=CARTESIAN_POINT ( 'NONE',  ( -70.04900473833201602, -225.0595978535631616, 79.55554317441176693 ) ) ;
#4754=ADVANCED_FACE ( 'NONE', ( #3404 ), #7582, .T. ) ;
#4763=EDGE_CURVE ( 'NONE', #4080, #3340, #582, .T. ) ;
#4769=VECTOR ( 'NONE', #3467, 1000.000000000000000 ) ;
#4772=EDGE_CURVE ( 'NONE', #5471, #5437, #3517, .T. ) ;
#4783=CARTESIAN_POINT ( 'NONE',  ( -53.29386626619290723, -223.8662738488881985, 73.49650827186496826 ) ) ;
#4785=CARTESIAN_POINT ( 'NONE',  ( -21.50000000000000000, -223.0630240738404950, 96.09122589815579829 ) ) ;
#4786=EDGE_CURVE ( 'NONE', #2388, #5318, #6682, .T. ) ;
#4788=EDGE_LOOP ( 'NONE', ( #5670, #1121 ) ) ;
#4795=VERTEX_POINT ( 'NONE', #5860 ) ;
#4804=DIRECTION ( 'NONE',  ( 2.465190328815661892E-32, 1.000000000000000000, 1.193489751472043281E-15 ) ) ;
#4807=CARTESIAN_POINT ( 'NONE',  ( -64.50000000000000000, -113.7796841263389211, 41.77968412633906325 ) ) ;
#4808=VECTOR ( 'NONE', #6018, 1000.000000000000114 ) ;
#4814=CARTESIAN_POINT ( 'NONE',  ( -53.03180245857092956, -218.0630240738404950, 71.94153218116483117 ) ) ;
#4815=CARTESIAN_POINT ( 'NONE',  ( -53.29386626619290723, -219.0153713307822443, 95.37751551101598579 ) ) ;
#4816=CARTESIAN_POINT ( 'NONE',  ( -70.25616595088855831, -213.3481074634626964, 88.53882300612518463 ) ) ;
#4818=CARTESIAN_POINT ( 'NONE',  ( -61.25564343853275773, -218.0630214440888608, 91.79691897930752020 ) ) ;
#4821=ORIENTED_EDGE ( 'NONE', *, *, #4688, .T. ) ;
#4830=ORIENTED_EDGE ( 'NONE', *, *, #1141, .F. ) ;
#4833=DIRECTION ( 'NONE',  ( -0.6444004775717536715, 0.5407162030609466985, -0.5407162030609483638 ) ) ;
#4840=ADVANCED_FACE ( 'NONE', ( #5165 ), #7505, .F. ) ;
#4844=CARTESIAN_POINT ( 'NONE',  ( -62.71099586730315423, -223.0636365687223872, 78.56832023356531636 ) ) ;
#4851=AXIS2_PLACEMENT_3D ( 'NONE', #5379, #2335, #7141 ) ;
#4856=CARTESIAN_POINT ( 'NONE',  ( -63.70683303208141268, -218.0630240594568647, 87.95135174290737723 ) ) ;
#4864=DIRECTION ( 'NONE',  ( -0.7071067811865436870, -8.465450562766819607E-16, 0.7071067811865514585 ) ) ;
#4870=DIRECTION ( 'NONE',  ( 3.081487911019577365E-33, 1.193489751472043281E-15, -1.000000000000000000 ) ) ;
#4876=( LENGTH_UNIT ( ) NAMED_UNIT ( * ) SI_UNIT ( .MILLI., .METRE. ) );
#4883=CARTESIAN_POINT ( 'NONE',  ( -60.84172821740799719, -223.0630987092885960, 76.30858369176860379 ) ) ;
#4893=CARTESIAN_POINT ( 'NONE',  ( -53.25168462842736261, -218.0630240738404950, 95.20959099461346398 ) ) ;
#4897=CARTESIAN_POINT ( 'NONE',  ( -24.15685424949240456, -63.34314575050749596, 36.34314575050759544 ) ) ;
#4910=DIRECTION ( 'NONE',  ( -2.465190328815661892E-32, -0.7071067811865484609, -0.7071067811865465735 ) ) ;
#4923=CARTESIAN_POINT ( 'NONE',  ( -53.10580595754475297, -219.7017882839731158, 72.38063772785491778 ) ) ;
#4927=DIRECTION ( 'NONE',  ( -9.244463733058732095E-33, -5.551115123125783935E-17, 1.000000000000000000 ) ) ;
#4929=CARTESIAN_POINT ( 'NONE',  ( -61.30885008117680712, -218.0630240738405519, 91.74137814073138486 ) ) ;
#4954=DIRECTION ( 'NONE',  ( 4.336808689942013792E-16, 0.000000000000000000, 1.000000000000000000 ) ) ;
#4956=CARTESIAN_POINT ( 'NONE',  ( -61.15513345216592000, -223.0630249525806903, 76.61458237095268942 ) ) ;
#4959=ORIENTED_EDGE ( 'NONE', *, *, #6801, .F. ) ;
#4965=FACE_OUTER_BOUND ( 'NONE', #2302, .T. ) ;
#4966=AXIS2_PLACEMENT_3D ( 'NONE', #2674, #3334, #6792 ) ;
#4971=AXIS2_PLACEMENT_3D ( 'NONE', #5264, #4804, #4153 ) ;
#4972=CARTESIAN_POINT ( 'NONE',  ( -26.50000000000003197, -60.68629150101524772, -11.31370849898474873 ) ) ;
#4974=ORIENTED_EDGE ( 'NONE', *, *, #4334, .T. ) ;
#4985=DIRECTION ( 'NONE',  ( 0.000000000000000000, 0.000000000000000000, 1.000000000000000000 ) ) ;
#4986=CARTESIAN_POINT ( 'NONE',  ( -24.81370849898475939, -223.0630240738404382, 73.28127814332046341 ) ) ;
#4999=CARTESIAN_POINT ( 'NONE',  ( -63.60023158588590064, -223.0630242615051202, 80.29653509657342170 ) ) ;
#5005=EDGE_LOOP ( 'NONE', ( #1213, #2651, #6283, #1063, #6483, #1480, #691, #5571 ) ) ;
#5006=CARTESIAN_POINT ( 'NONE',  ( -21.50000000000000000, -120.9522879036833558, 45.92078884797942351 ) ) ;
#5011=ORIENTED_EDGE ( 'NONE', *, *, #1072, .T. ) ;
#5013=DIRECTION ( 'NONE',  ( 2.465190328815662439E-32, 0.7071067811865465735, -0.7071067811865485719 ) ) ;
#5017=ORIENTED_EDGE ( 'NONE', *, *, #3884, .T. ) ;
#5019=CARTESIAN_POINT ( 'NONE',  ( -21.49999999999999645, -219.7493155748557285, 72.39337262706536080 ) ) ;
#5021=CARTESIAN_POINT ( 'NONE',  ( -53.17910001414513488, -216.4242598635583477, 94.92063264932129130 ) ) ;
#5028=CARTESIAN_POINT ( 'NONE',  ( -60.84337381445615733, -223.0630240738404950, 93.24745791952346963 ) ) ;
#5034=CARTESIAN_POINT ( 'NONE',  ( -24.81370849898475583, -223.0630240738404382, 96.09122589815579829 ) ) ;
#5046=CARTESIAN_POINT ( 'NONE',  ( -21.50563895418471461, -113.9621117585880512, 41.96211175858820042 ) ) ;
#5048=VERTEX_POINT ( 'NONE', #4897 ) ;
#5049=FACE_OUTER_BOUND ( 'NONE', #4633, .T. ) ;
#5050=CARTESIAN_POINT ( 'NONE',  ( -29.50000000000000000, -223.0630240738404950, 73.28127814332044920 ) ) ;
#5053=CARTESIAN_POINT ( 'NONE',  ( -53.01709100512436379, -212.7665347604136912, 94.27567702562228646 ) ) ;
#5057=ORIENTED_EDGE ( 'NONE', *, *, #5945, .F. ) ;
#5062=CARTESIAN_POINT ( 'NONE',  ( -61.57753664718645581, -223.0629867915132536, 92.46999602602490143 ) ) ;
#5065=CARTESIAN_POINT ( 'NONE',  ( -57.45460281882250797, -218.0630240738404666, 72.85609881942959021 ) ) ;
#5067=EDGE_LOOP ( 'NONE', ( #1582, #3883, #6387, #2804 ) ) ;
#5070=LINE ( 'NONE', #6298, #5832 ) ;
#5071=CARTESIAN_POINT ( 'NONE',  ( -29.49999999999998934, 16.00000000000004263, 42.31370849898485886 ) ) ;
#5075=ORIENTED_EDGE ( 'NONE', *, *, #181, .T. ) ;
#5092=CARTESIAN_POINT ( 'NONE',  ( -52.98766809822284785, -212.1022451272887110, 94.15854484029739524 ) ) ;
#5106=CARTESIAN_POINT ( 'NONE',  ( -63.72956387582338778, -223.0630239280731928, 88.95744984476777972 ) ) ;
#5112=CARTESIAN_POINT ( 'NONE',  ( -32.50000000000002842, -60.68629150101523351, -11.31370849898474873 ) ) ;
#5132=CARTESIAN_POINT ( 'NONE',  ( -53.06880420804608889, -213.9340789708228954, 94.48154657108737808 ) ) ;
#5133=CARTESIAN_POINT ( 'NONE',  ( -32.50000000000002132, -45.34314575050759544, 18.34314575050763452 ) ) ;
#5138=EDGE_CURVE ( 'NONE', #4666, #7513, #2001, .T. ) ;
#5141=CARTESIAN_POINT ( 'NONE',  ( -26.50000000000000711, -71.76505905230354188, 44.76505905230365556 ) ) ;
#5145=CARTESIAN_POINT ( 'NONE',  ( -64.34713424250860214, -218.0649563631192223, 81.64184023509517374 ) ) ;
#5156=LINE ( 'NONE', #6053, #7580 ) ;
#5160=ORIENTED_EDGE ( 'NONE', *, *, #4082, .F. ) ;
#5164=EDGE_CURVE ( 'NONE', #208, #2155, #7345, .T. ) ;
#5165=FACE_OUTER_BOUND ( 'NONE', #1135, .T. ) ;
#5167=ORIENTED_EDGE ( 'NONE', *, *, #3954, .F. ) ;
#5171=PLANE ( 'NONE',  #2993 ) ;
#5174=AXIS2_PLACEMENT_3D ( 'NONE', #5815, #1694, #1149 ) ;
#5176=EDGE_CURVE ( 'NONE', #3850, #208, #3578, .T. ) ;
#5179=CYLINDRICAL_SURFACE ( 'NONE', #6311, 15.99999999999999645 ) ;
#5180=LINE ( 'NONE', #3529, #3696 ) ;
#5184=CARTESIAN_POINT ( 'NONE',  ( -59.96426363863164255, -218.0635656269040510, 74.31118017701729173 ) ) ;
#5192=ORIENTED_EDGE ( 'NONE', *, *, #6532, .T. ) ;
#5194=CARTESIAN_POINT ( 'NONE',  ( -26.49999999999999289, -216.4061698243480976, 71.49757942303730829 ) ) ;
#5200=EDGE_LOOP ( 'NONE', ( #5385, #3732, #806, #4257 ) ) ;
#5207=DIRECTION ( 'NONE',  ( 3.697785493223493385E-32, 0.7071067811865485719, 0.7071067811865464625 ) ) ;
#5209=EDGE_CURVE ( 'NONE', #2155, #1164, #3378, .T. ) ;
#5210=ORIENTED_EDGE ( 'NONE', *, *, #1141, .T. ) ;
#5220=CARTESIAN_POINT ( 'NONE',  ( -61.32863543632851133, -218.0630603687720281, 75.59213739089364026 ) ) ;
#5223=AXIS2_PLACEMENT_3D ( 'NONE', #2732, #1498, #6817 ) ;
#5241=ORIENTED_EDGE ( 'NONE', *, *, #6910, .T. ) ;
#5244=DIRECTION ( 'NONE',  ( 1.000000000000000000, 2.465190328815661892E-32, -9.244463733058732095E-33 ) ) ;
#5257=CARTESIAN_POINT ( 'NONE',  ( -21.50000000000000000, -114.3401965514817960, 42.31370849898471675 ) ) ;
#5264=CARTESIAN_POINT ( 'NONE',  ( -64.50000000000000000, -223.0630240738404950, 73.28127814332044920 ) ) ;
#5267=DIRECTION ( 'NONE',  ( -2.465190328815661892E-32, -1.000000000000000000, -1.193489751472043281E-15 ) ) ;
#5271=ORIENTED_EDGE ( 'NONE', *, *, #6333, .T. ) ;
#5293=PRODUCT ( 'right arm', 'right arm', '', ( #5863 ) ) ;
#5307=CYLINDRICAL_SURFACE ( 'NONE', #1897, 6.000000000000000000 ) ;
#5309=CARTESIAN_POINT ( 'NONE',  ( -53.00237955168407922, -217.4114710059382674, 71.76694906279446684 ) ) ;
#5318=VERTEX_POINT ( 'NONE', #7574 ) ;
#5320=CARTESIAN_POINT ( 'NONE',  ( -30.49999999999998579, -214.0630240738404666, 96.09122589815579829 ) ) ;
#5336=ORIENTED_EDGE ( 'NONE', *, *, #3100, .T. ) ;
#5352=CARTESIAN_POINT ( 'NONE',  ( -26.50000000000000711, -125.0933926253236450, 30.46597562735434295 ) ) ;
#5356=CARTESIAN_POINT ( 'NONE',  ( -60.68960140267981274, -218.8824061789508733, 72.16108495452549221 ) ) ;
#5357=LINE ( 'NONE', #86, #502 ) ;
#5360=ORIENTED_EDGE ( 'NONE', *, *, #363, .F. ) ;
#5362=CARTESIAN_POINT ( 'NONE',  ( -26.50000000000003197, 0.000000000000000000, 0.000000000000000000 ) ) ;
#5367=CARTESIAN_POINT ( 'NONE',  ( -64.50000000000000000, -60.68629150101525482, -11.31370849898474873 ) ) ;
#5368=ORIENTED_EDGE ( 'NONE', *, *, #2252, .F. ) ;
#5372=VERTEX_POINT ( 'NONE', #6967 ) ;
#5379=CARTESIAN_POINT ( 'NONE',  ( -29.50000000000000000, -215.0630240738404950, 73.28127814332047762 ) ) ;
#5382=CARTESIAN_POINT ( 'NONE',  ( -32.50000000000002842, -60.68629150101524772, -11.31370849898474873 ) ) ;
#5385=ORIENTED_EDGE ( 'NONE', *, *, #2252, .T. ) ;
#5386=ADVANCED_FACE ( 'NONE', ( #4746 ), #5307, .F. ) ;
#5387=ORIENTED_EDGE ( 'NONE', *, *, #1352, .T. ) ;
#5389=CARTESIAN_POINT ( 'NONE',  ( -53.25365409304692577, -218.1074892565141283, 95.21743140602096389 ) ) ;
#5391=CARTESIAN_POINT ( 'NONE',  ( -70.24145449743711822, -214.0092129552773201, 88.67031792470811524 ) ) ;
#5393=CARTESIAN_POINT ( 'NONE',  ( -57.20103464615607436, -218.0628873493838000, 94.48139145718995735 ) ) ;
#5394=VERTEX_POINT ( 'NONE', #2346 ) ;
#5408=CARTESIAN_POINT ( 'NONE',  ( -32.50000000000002842, 16.00000000000012079, -15.99999999999995914 ) ) ;
#5416=CYLINDRICAL_SURFACE ( 'NONE', #3411, 8.000000000000007105 ) ;
#5424=EDGE_CURVE ( 'NONE', #5460, #1413, #6788, .T. ) ;
#5427=DIRECTION ( 'NONE',  ( 0.000000000000000000, 0.000000000000000000, 1.000000000000000000 ) ) ;
#5428=CARTESIAN_POINT ( 'NONE',  ( -70.12317295347672541, -221.7587214059827261, 78.74778750054862542 ) ) ;
#5430=CARTESIAN_POINT ( 'NONE',  ( -56.75063899659176059, -218.0625894763260817, 94.64364256205048775 ) ) ;
#5437=VERTEX_POINT ( 'NONE', #1263 ) ;
#5438=EDGE_CURVE ( 'NONE', #2174, #5858, #6321, .T. ) ;
#5455=CARTESIAN_POINT ( 'NONE',  ( -64.34084354375256964, -223.0645981545465588, 82.82631477277033127 ) ) ;
#5460=VERTEX_POINT ( 'NONE', #7192 ) ;
#5467=CARTESIAN_POINT ( 'NONE',  ( -53.50256896896199521, -228.4878731603045026, 74.73486207509921542 ) ) ;
#5468=DIRECTION ( 'NONE',  ( -9.244463733058732095E-33, -4.557872517964703399E-64, -1.000000000000000000 ) ) ;
#5470=CARTESIAN_POINT ( 'NONE',  ( -58.28420576404219133, -218.0630240738404382, 94.02398971667126659 ) ) ;
#5471=VERTEX_POINT ( 'NONE', #3507 ) ;
#5472=AXIS2_PLACEMENT_3D ( 'NONE', #6847, #2156, #3396 ) ;
#5485=LINE ( 'NONE', #708, #3009 ) ;
#5488=PLANE ( 'NONE',  #6392 ) ;
#5494=CARTESIAN_POINT ( 'NONE',  ( -64.08458520774711076, -223.0616687716003241, 87.89351621351769950 ) ) ;
#5500=ADVANCED_FACE ( 'NONE', ( #6689 ), #6729, .F. ) ;
#5503=CARTESIAN_POINT ( 'NONE',  ( -23.84314575050760965, -108.6568542494922127, 36.65685424949233351 ) ) ;
#5506=CARTESIAN_POINT ( 'NONE',  ( -64.49232742940240826, -218.0627193185516433, 84.13172309758257938 ) ) ;
#5516=CARTESIAN_POINT ( 'NONE',  ( -31.48397095257175238, -108.8525495989622414, 36.85254959896238347 ) ) ;
#5525=CARTESIAN_POINT ( 'NONE',  ( -64.50000000000000000, -223.0630240738404950, 96.09122589815579829 ) ) ;
#5528=CARTESIAN_POINT ( 'NONE',  ( -63.90555473623476956, -223.0625582585724942, 88.46971898607593232 ) ) ;
#5543=VERTEX_POINT ( 'NONE', #1484 ) ;
#5554=CYLINDRICAL_SURFACE ( 'NONE', #6183, 8.000000000000017764 ) ;
#5568=CARTESIAN_POINT ( 'NONE',  ( -61.18228816775778256, -223.0630240738406087, 76.64217870502731955 ) ) ;
#5571=ORIENTED_EDGE ( 'NONE', *, *, #5209, .T. ) ;
#5580=AXIS2_PLACEMENT_3D ( 'NONE', #349, #3284, #4985 ) ;
#5584=ORIENTED_EDGE ( 'NONE', *, *, #2936, .T. ) ;
#5589=VECTOR ( 'NONE', #6855, 1000.000000000000000 ) ;
#5590=ORIENTED_EDGE ( 'NONE', *, *, #1442, .F. ) ;
#5592=AXIS2_PLACEMENT_3D ( 'NONE', #6799, #3306, #411 ) ;
#5593=VECTOR ( 'NONE', #6216, 1000.000000000000000 ) ;
#5597=VECTOR ( 'NONE', #7291, 1000.000000000000000 ) ;
#5599=CARTESIAN_POINT ( 'NONE',  ( -60.75187451922243298, -218.1519544391847489, 95.22527181742795221 ) ) ;
#5601=( NAMED_UNIT ( * ) PLANE_ANGLE_UNIT ( ) SI_UNIT ( $, .RADIAN. ) );
#5603=ORIENTED_EDGE ( 'NONE', *, *, #6472, .T. ) ;
#5608=FACE_OUTER_BOUND ( 'NONE', #7043, .T. ) ;
#5625=ORIENTED_EDGE ( 'NONE', *, *, #7493, .T. ) ;
#5629=CARTESIAN_POINT ( 'NONE',  ( -53.25365409304695419, -218.1074892565148389, 95.21743140602109179 ) ) ;
#5637=CARTESIAN_POINT ( 'NONE',  ( -53.03180245857092956, -218.0630240738404950, 71.94153218116483117 ) ) ;
#5643=EDGE_CURVE ( 'NONE', #5778, #920, #1409, .T. ) ;
#5650=VECTOR ( 'NONE', #3951, 1000.000000000000000 ) ;
#5655=VECTOR ( 'NONE', #1258, 1000.000000000000000 ) ;
#5659=DIRECTION ( 'NONE',  ( -2.465190328815661892E-32, -1.000000000000000000, -1.193489751472043281E-15 ) ) ;
#5665=CARTESIAN_POINT ( 'NONE',  ( -29.50000000000000000, -223.0630240738404950, 73.28127814332044920 ) ) ;
#5670=ORIENTED_EDGE ( 'NONE', *, *, #4786, .F. ) ;
#5671=ORIENTED_EDGE ( 'NONE', *, *, #6532, .F. ) ;
#5678=CARTESIAN_POINT ( 'NONE',  ( -57.86411036119383056, -223.0630208489766915, 95.16303203405658451 ) ) ;
#5685=ORIENTED_EDGE ( 'NONE', *, *, #2314, .F. ) ;
#5706=CYLINDRICAL_SURFACE ( 'NONE', #3222, 7.999999999999986677 ) ;
#5720=CARTESIAN_POINT ( 'NONE',  ( -61.39066111053622166, -223.0630240738405234, 92.67132228217317902 ) ) ;
#5731=CARTESIAN_POINT ( 'NONE',  ( -24.15685424949240456, -63.34314575050749596, 36.34314575050759544 ) ) ;
#5746=ADVANCED_FACE ( 'NONE', ( #4041 ), #7565, .F. ) ;
#5751=DIRECTION ( 'NONE',  ( 1.000000000000000000, 2.465190328815661892E-32, -9.244463733058732095E-33 ) ) ;
#5753=CARTESIAN_POINT ( 'NONE',  ( -31.48397095257174527, -63.85254959896236215, 36.85254959896246874 ) ) ;
#5762=CARTESIAN_POINT ( 'NONE',  ( -63.27290876320206081, -218.0630240738404666, 78.35050765050191046 ) ) ;
#5778=VERTEX_POINT ( 'NONE', #6572 ) ;
#5788=DIRECTION ( 'NONE',  ( -1.000000000000000000, -2.465190328815661892E-32, -9.244463733058733463E-33 ) ) ;
#5790=ORIENTED_EDGE ( 'NONE', *, *, #4461, .F. ) ;
#5799=CARTESIAN_POINT ( 'NONE',  ( -63.67751884086511893, -218.0631193926485309, 79.33280772544384263 ) ) ;
#5815=CARTESIAN_POINT ( 'NONE',  ( -21.49999999999999645, -125.0933926253236450, 30.46597562735434295 ) ) ;
#5817=ORIENTED_EDGE ( 'NONE', *, *, #3868, .T. ) ;
#5828=EDGE_CURVE ( 'NONE', #4634, #1071, #6536, .T. ) ;
#5832=VECTOR ( 'NONE', #2716, 1000.000000000000114 ) ;
#5837=LINE ( 'NONE', #4068, #6880 ) ;
#5838=VECTOR ( 'NONE', #5013, 1000.000000000000000 ) ;
#5841=ORIENTED_EDGE ( 'NONE', *, *, #4544, .T. ) ;
#5846=AXIS2_PLACEMENT_3D ( 'NONE', #1316, #3675, #4870 ) ;
#5856=LINE ( 'NONE', #7001, #4620 ) ;
#5858=VERTEX_POINT ( 'NONE', #719 ) ;
#5859=AXIS2_PLACEMENT_3D ( 'NONE', #5071, #4389, #6798 ) ;
#5860=CARTESIAN_POINT ( 'NONE',  ( -32.50000000000002842, -49.37258300203047412, -6.000000000000002665 ) ) ;
#5863=PRODUCT_CONTEXT ( 'NONE', #106, 'mechanical' ) ;
#5887=CARTESIAN_POINT ( 'NONE',  ( -70.16044999292957129, -220.0996966972331848, 78.34180846956243727 ) ) ;
#5889=EDGE_CURVE ( 'NONE', #917, #920, #3497, .T. ) ;
#5908=ORIENTED_EDGE ( 'NONE', *, *, #4594, .T. ) ;
#5909=ORIENTED_EDGE ( 'NONE', *, *, #3271, .T. ) ;
#5925=CARTESIAN_POINT ( 'NONE',  ( -60.77671317003689211, -224.6695236240148290, 73.71173840043843484 ) ) ;
#5926=CARTESIAN_POINT ( 'NONE',  ( -21.49999999999999289, -67.16361968246712877, 40.16361968246722824 ) ) ;
#5930=( BOUNDED_CURVE ( )  B_SPLINE_CURVE ( 3, ( #5050, #4986, #5019, #7470 ),
 .UNSPECIFIED., .F., .T. ) 
 B_SPLINE_CURVE_WITH_KNOTS ( ( 4, 4 ),
 ( 3.141592653589793116, 4.712388980384689674 ),
 .UNSPECIFIED. ) 
 CURVE ( )  GEOMETRIC_REPRESENTATION_ITEM ( )  RATIONAL_B_SPLINE_CURVE ( ( 1.000000000000000000, 0.8047378541243649375, 0.8047378541243649375, 1.000000000000000000 ) ) 
 REPRESENTATION_ITEM ( '' )  );
#5945=EDGE_CURVE ( 'NONE', #3412, #5460, #6588, .T. ) ;
#5948=DIRECTION ( 'NONE',  ( 1.000000000000000000, 2.465190328815661892E-32, -9.244463733058732095E-33 ) ) ;
#5965=CARTESIAN_POINT ( 'NONE',  ( -60.82928583850154780, -228.1620966263574246, 74.64757051591659831 ) ) ;
#5966=ADVANCED_FACE ( 'NONE', ( #978 ), #2134, .F. ) ;
#5967=CARTESIAN_POINT ( 'NONE',  ( -57.48968592151182833, -218.0630067422592617, 94.36623590530653871 ) ) ;
#5973=DIRECTION ( 'NONE',  ( 0.000000000000000000, 0.000000000000000000, -1.000000000000000000 ) ) ;
#5974=ORIENTED_EDGE ( 'NONE', *, *, #2936, .F. ) ;
#5977=EDGE_CURVE ( 'NONE', #4634, #2155, #6831, .T. ) ;
#5978=ADVANCED_FACE ( 'NONE', ( #3914 ), #5179, .T. ) ;
#5999=ADVANCED_FACE ( 'NONE', ( #5608 ), #331, .F. ) ;
#6001=CARTESIAN_POINT ( 'NONE',  ( -21.50000000000000000, -105.5631177942458407, 67.24940929526130162 ) ) ;
#6004=CARTESIAN_POINT ( 'NONE',  ( -59.85703050705383532, -218.0624546635179399, 93.03239386934940569 ) ) ;
#6011=FACE_OUTER_BOUND ( 'NONE', #127, .T. ) ;
#6012=CARTESIAN_POINT ( 'NONE',  ( -32.50000000000002842, -49.37258300203047412, -15.99999999999998579 ) ) ;
#6017=CARTESIAN_POINT ( 'NONE',  ( -27.07790214619733860, -113.7796841263389069, 41.77968412633906325 ) ) ;
#6018=DIRECTION ( 'NONE',  ( -5.868966822792461377E-17, 0.9848077530122080203, -0.1736481776669304422 ) ) ;
#6024=AXIS2_PLACEMENT_3D ( 'NONE', #6338, #1675, #4606 ) ;
#6026=DIRECTION ( 'NONE',  ( 1.000000000000000000, 2.465190328815661892E-32, -9.244463733058732095E-33 ) ) ;
#6031=CARTESIAN_POINT ( 'NONE',  ( -63.60636663337245267, -223.0630240873432797, 80.31129794962551216 ) ) ;
#6032=DIRECTION ( 'NONE',  ( 1.000000000000000000, 2.465190328815661892E-32, -9.244463733058732095E-33 ) ) ;
#6040=CARTESIAN_POINT ( 'NONE',  ( -60.80066350777958206, -226.2606222968802854, 74.13807200489549132 ) ) ;
#6042=DIRECTION ( 'NONE',  ( -2.465190328815661892E-32, -1.000000000000000000, -1.193489751472043281E-15 ) ) ;
#6053=CARTESIAN_POINT ( 'NONE',  ( -64.50000000000000000, -104.1739323729103575, 75.12787131935894536 ) ) ;
#6055=ORIENTED_EDGE ( 'NONE', *, *, #3544, .T. ) ;
#6061=CIRCLE ( 'NONE', #7166, 6.000000000000000888 ) ;
#6065=CARTESIAN_POINT ( 'NONE',  ( -56.68590668195482607, -223.0634275682792236, 73.83207632951022958 ) ) ;
#6067=VECTOR ( 'NONE', #2790, 1000.000000000000000 ) ;
#6070=ORIENTED_EDGE ( 'NONE', *, *, #5424, .F. ) ;
#6078=CARTESIAN_POINT ( 'NONE',  ( -63.70849213729819382, -218.0630240738405519, 87.94705950315832865 ) ) ;
#6083=CARTESIAN_POINT ( 'NONE',  ( -26.50000000000003197, -102.6862915010150346, 30.68629150101517666 ) ) ;
#6104=CARTESIAN_POINT ( 'NONE',  ( -61.17229153618341542, -223.0630242530635883, 76.63199592159693907 ) ) ;
#6105=ORIENTED_EDGE ( 'NONE', *, *, #4772, .T. ) ;
#6114=CARTESIAN_POINT ( 'NONE',  ( -26.50000000000003197, -7.347880794884112834E-16, -6.000000000000001776 ) ) ;
#6127=ORIENTED_EDGE ( 'NONE', *, *, #1870, .T. ) ;
#6129=DIRECTION ( 'NONE',  ( -7.623657272262513435E-17, 0.7071067811865465735, -0.7071067811865484609 ) ) ;
#6136=CARTESIAN_POINT ( 'NONE',  ( -64.17143802327697699, -223.0612697797253361, 87.56774190916064526 ) ) ;
#6153=ORIENTED_EDGE ( 'NONE', *, *, #3681, .T. ) ;
#6155=EDGE_CURVE ( 'NONE', #3340, #4643, #4364, .T. ) ;
#6165=EDGE_LOOP ( 'NONE', ( #876, #5011, #5167, #4468, #3516, #69, #1734 ) ) ;
#6169=CARTESIAN_POINT ( 'NONE',  ( -32.50000000000002842, -49.37258300203047412, 6.000000000000000888 ) ) ;
#6170=CARTESIAN_POINT ( 'NONE',  ( -60.48402471930579338, -223.0632605723740767, 75.98548927210011072 ) ) ;
#6176=EDGE_CURVE ( 'NONE', #1843, #3503, #5070, .T. ) ;
#6178=CARTESIAN_POINT ( 'NONE',  ( -26.49999999999999645, -99.90626354475344328, 72.90626354475362803 ) ) ;
#6179=VECTOR ( 'NONE', #6369, 1000.000000000000000 ) ;
#6183=AXIS2_PLACEMENT_3D ( 'NONE', #964, #4436, #7387 ) ;
#6190=CIRCLE ( 'NONE', #1898, 15.99999999999998934 ) ;
#6194=AXIS2_PLACEMENT_3D ( 'NONE', #3897, #5659, #2728 ) ;
#6200=CARTESIAN_POINT ( 'NONE',  ( -53.25562355766778921, -218.1519544391847774, 95.22527181742790958 ) ) ;
#6207=( GEOMETRIC_REPRESENTATION_CONTEXT ( 3 ) GLOBAL_UNCERTAINTY_ASSIGNED_CONTEXT ( ( #3490 ) ) GLOBAL_UNIT_ASSIGNED_CONTEXT ( ( #743, #820, #7283 ) ) REPRESENTATION_CONTEXT ( 'NONE', 'WORKASPACE' ) );
#6212=CARTESIAN_POINT ( 'NONE',  ( -58.17782861558893615, -223.0629528839427564, 95.01857375712019405 ) ) ;
#6216=DIRECTION ( 'NONE',  ( 1.000000000000000000, 2.465190328815661892E-32, -9.244463733058732095E-33 ) ) ;
#6219=CARTESIAN_POINT ( 'NONE',  ( -21.50000000000000000, -215.0630240738404950, 94.68061005248806339 ) ) ;
#6222=DIRECTION ( 'NONE',  ( -2.465190328815662439E-32, -1.000000000000000000, -5.551115123125783935E-17 ) ) ;
#6223=CIRCLE ( 'NONE', #1186, 8.000000000000007105 ) ;
#6227=ADVANCED_FACE ( 'NONE', ( #2450 ), #112, .F. ) ;
#6240=CARTESIAN_POINT ( 'NONE',  ( -60.66255603274095165, -212.1022451272887110, 94.15854484029743787 ) ) ;
#6245=ADVANCED_FACE ( 'NONE', ( #7597 ), #3032, .T. ) ;
#6252=CARTESIAN_POINT ( 'NONE',  ( -29.50000000000000000, -223.0630240738404950, 96.09122589815579829 ) ) ;
#6253=EDGE_LOOP ( 'NONE', ( #2343, #5017, #5241, #2143 ) ) ;
#6263=ORIENTED_EDGE ( 'NONE', *, *, #2678, .F. ) ;
#6265=CLOSED_SHELL ( 'NONE', ( #5999, #3150, #2860, #3900, #5978, #1242, #2818, #3806, #1395, #1299, #6227, #5500, #5966, #4061, #4754, #2924, #4285, #5746, #4671, #804, #4840, #6899, #2375, #6987, #4402, #2113, #4706, #5386, #6245, #740 ) ) ;
#6280=CARTESIAN_POINT ( 'NONE',  ( -70.00607124224620748, -224.5869008243856797, 90.77423662209318422 ) ) ;
#6281=CARTESIAN_POINT ( 'NONE',  ( -30.49999999999998579, -218.0630240738404950, 95.20959099461346398 ) ) ;
#6283=ORIENTED_EDGE ( 'NONE', *, *, #2945, .T. ) ;
#6288=DIRECTION ( 'NONE',  ( 0.000000000000000000, 0.000000000000000000, 1.000000000000000000 ) ) ;
#6294=CARTESIAN_POINT ( 'NONE',  ( -53.75100615578827501, -218.0630240738404950, 71.94153218116485959 ) ) ;
#6298=CARTESIAN_POINT ( 'NONE',  ( -26.50000000000000355, -120.9522879036833558, 45.92078884797942351 ) ) ;
#6299=CARTESIAN_POINT ( 'NONE',  ( -53.25365409304696840, -222.9757987891380253, 73.25790619872483944 ) ) ;
#6307=ORIENTED_EDGE ( 'NONE', *, *, #2677, .F. ) ;
#6311=AXIS2_PLACEMENT_3D ( 'NONE', #6950, #1674, #6375 ) ;
#6313=CARTESIAN_POINT ( 'NONE',  ( -26.50000000000000000, -69.36092951174981636, 42.36092951174991583 ) ) ;
#6321=CIRCLE ( 'NONE', #794, 8.000000000000007105 ) ;
#6322=FACE_OUTER_BOUND ( 'NONE', #5200, .T. ) ;
#6333=EDGE_CURVE ( 'NONE', #5437, #2475, #291, .T. ) ;
#6338=CARTESIAN_POINT ( 'NONE',  ( -32.50000000000002842, 6.938893903907228378E-15, 0.000000000000000000 ) ) ;
#6341=CARTESIAN_POINT ( 'NONE',  ( -61.15478436381093275, -218.0630249522653514, 75.41002070443643390 ) ) ;
#6356=ORIENTED_EDGE ( 'NONE', *, *, #4688, .F. ) ;
#6367=CIRCLE ( 'NONE', #3051, 15.99999999999997335 ) ;
#6369=DIRECTION ( 'NONE',  ( 1.000000000000000000, 2.465190328815661892E-32, -9.244463733058732095E-33 ) ) ;
#6373=DIRECTION ( 'NONE',  ( -1.000000000000000000, -1.725633230170963324E-31, 1.078147950931789387E-16 ) ) ;
#6375=DIRECTION ( 'NONE',  ( 0.000000000000000000, 0.000000000000000000, 1.000000000000000000 ) ) ;
#6379=CARTESIAN_POINT ( 'NONE',  ( -57.83326664796290117, -218.0630925741273813, 73.02699328150956148 ) ) ;
#6387=ORIENTED_EDGE ( 'NONE', *, *, #4232, .T. ) ;
#6391=ORIENTED_EDGE ( 'NONE', *, *, #1870, .F. ) ;
#6392=AXIS2_PLACEMENT_3D ( 'NONE', #249, #4910, #7246 ) ;
#6400=ORIENTED_EDGE ( 'NONE', *, *, #5138, .T. ) ;
#6406=ORIENTED_EDGE ( 'NONE', *, *, #7381, .F. ) ;
#6432=ORIENTED_EDGE ( 'NONE', *, *, #5138, .F. ) ;
#6440=CARTESIAN_POINT ( 'NONE',  ( -26.49999999999999645, -104.1739323729103859, 75.12787131935894536 ) ) ;
#6442=VECTOR ( 'NONE', #2240, 1000.000000000000000 ) ;
#6449=DIRECTION ( 'NONE',  ( -2.465190328815661892E-32, -1.000000000000000000, -1.193489751472043281E-15 ) ) ;
#6450=EDGE_CURVE ( 'NONE', #7540, #2908, #2366, .T. ) ;
#6468=ORIENTED_EDGE ( 'NONE', *, *, #4051, .T. ) ;
#6469=CARTESIAN_POINT ( 'NONE',  ( -70.14230383934500423, -218.4648600334252535, 89.55655311265203977 ) ) ;
#6472=EDGE_CURVE ( 'NONE', #2971, #1164, #1170, .T. ) ;
#6482=CIRCLE ( 'NONE', #3773, 6.000000000000000000 ) ;
#6483=ORIENTED_EDGE ( 'NONE', *, *, #4361, .T. ) ;
#6507=CARTESIAN_POINT ( 'NONE',  ( -60.83418965632457542, -228.4878731603066910, 74.73486207509363055 ) ) ;
#6509=DIRECTION ( 'NONE',  ( -4.930380657631323236E-32, -0.9848077530122080203, 0.1736481776669304422 ) ) ;
#6517=CYLINDRICAL_SURFACE ( 'NONE', #2832, 4.000000000000003553 ) ;
#6532=EDGE_CURVE ( 'NONE', #4282, #4634, #6190, .T. ) ;
#6536=LINE ( 'NONE', #5382, #3371 ) ;
#6539=LINE ( 'NONE', #4807, #5655 ) ;
#6544=DIRECTION ( 'NONE',  ( 0.000000000000000000, 0.000000000000000000, 1.000000000000000000 ) ) ;
#6548=CARTESIAN_POINT ( 'NONE',  ( -69.99871551551807158, -227.2977332969690849, 80.10323607719463723 ) ) ;
#6549=CARTESIAN_POINT ( 'NONE',  ( -23.84314575050760965, -63.65685424949226956, 36.65685424949239035 ) ) ;
#6555=ORIENTED_EDGE ( 'NONE', *, *, #5438, .F. ) ;
#6567=FACE_OUTER_BOUND ( 'NONE', #2879, .T. ) ;
#6572=CARTESIAN_POINT ( 'NONE',  ( -21.51784377693468642, -113.7796841263389069, 41.77968412633906325 ) ) ;
#6582=CARTESIAN_POINT ( 'NONE',  ( -53.25365409304696129, -222.9757987891379685, 73.25790619872482523 ) ) ;
#6584=CARTESIAN_POINT ( 'NONE',  ( -63.64218808964506024, -218.0630119241219802, 88.11533740162713002 ) ) ;
#6588=B_SPLINE_CURVE_WITH_KNOTS ( 'NONE', 3,
 ( #7333, #6752, #2025, #257, #149, #6065, #862, #3801, #1365, #3727, #3764, #1476, #1984, #792, #3839, #2598, #3219, #6170, #2487, #4883, #4265, #902, #4382, #4956, #6104, #5568, #2063, #293, #4844, #3260, #6679, #7256, #7180, #1913, #6608, #224, #6720, #4999, #1330, #6031, #827, #753, #3180, #3106, #5455, #185, #1445, #7292, #2530, #3144, #2639, #6136, #5494, #2562, #5528, #7220, #4338, #1948, #4300, #6643, #1057, #5106, #7517, #2178, #2710, #4605, #7480, #2747, #4531, #478, #446, #5062, #6868, #4031, #6906, #7400, #5720, #5028, #3876, #1552, #1626, #4567, #7366, #6212, #364, #1588, #5678, #944, #2218, #3296, #1512, #4448, #401, #3988 ),
 .UNSPECIFIED., .F., .F.,
 ( 4, 2, 2, 2, 1, 1, 2, 2, 2, 2, 2, 1, 1, 1, 2, 2, 2, 2, 2, 1, 1, 1, 1, 1, 2, 2, 2, 2, 2, 2, 2, 2, 2, 1, 1, 1, 1, 1, 2, 2, 2, 2, 2, 1, 1, 1, 2, 2, 2, 2, 2, 1, 1, 2, 2, 2, 4 ),
 ( 0.000000000000000000, 0.06249999999992246480, 0.09374999999988342658, 0.1093749999998637201, 0.1171874999998538669, 0.1210937499998489403, 0.1230468749998462619, 0.1249999999998435696, 0.1874999999997534750, 0.2187499999997080669, 0.2343749999996855016, 0.2421874999996742328, 0.2460937499996684041, 0.2480468749996652678, 0.2490234374996635469, 0.2499999999996617983, 0.3124999999995126121, 0.3437499999994378941, 0.3593749999994005351, 0.3671874999993818278, 0.3710937499993730015, 0.3730468749993685607, 0.3740234374993658406, 0.3745117187493651745, 0.3747558593743645639, 0.3749999999993639532, 0.4374999999993808841, 0.4687499999993893218, 0.4843749999993939848, 0.4999999999993987032, 0.5624999999994173550, 0.5937499999994271249, 0.6093749999994321209, 0.6171874999994338973, 0.6210937499994346744, 0.6230468749994342303, 0.6240234374994351185, 0.6245117187494356736, 0.6247558593744355626, 0.6249999999994354516, 0.6874999999995098365, 0.7187499999995470290, 0.7343749999995660138, 0.7421874999995753397, 0.7460937499995802247, 0.7480468749995824451, 0.7490234374995835553, 0.7499999999995846656, 0.8124999999996914690, 0.8437499999997449818, 0.8593749999997714051, 0.8671874999997841726, 0.8710937499997907230, 0.8730468749997941647, 0.8749999999997974953, 0.9374999999998987477, 1.000000000000000000 ),
 .UNSPECIFIED. ) ;
#6593=PLANE ( 'NONE',  #5846 ) ;
#6597=CARTESIAN_POINT ( 'NONE',  ( -21.50000000000000000, -120.9522879036833558, 45.92078884797940219 ) ) ;
#6608=CARTESIAN_POINT ( 'NONE',  ( -63.53936842674539065, -223.0630354780872437, 80.15265254803479422 ) ) ;
#6615=CARTESIAN_POINT ( 'NONE',  ( -70.10306686690893230, -220.2280969603149572, 89.90726370123083200 ) ) ;
#6617=CARTESIAN_POINT ( 'NONE',  ( -63.38652985050246969, -218.0628171002711611, 88.70467567798203845 ) ) ;
#6619=ORIENTED_EDGE ( 'NONE', *, *, #2199, .T. ) ;
#6622=DIRECTION ( 'NONE',  ( -0.7071067811865513475, 0.000000000000000000, -0.7071067811865435759 ) ) ;
#6624=EDGE_CURVE ( 'NONE', #4643, #6889, #2623, .T. ) ;
#6633=MECHANICAL_DESIGN_GEOMETRIC_PRESENTATION_REPRESENTATION('',(#3568),#2084);
#6637=ORIENTED_EDGE ( 'NONE', *, *, #1954, .F. ) ;
#6640=FACE_OUTER_BOUND ( 'NONE', #7379, .T. ) ;
#6643=CARTESIAN_POINT ( 'NONE',  ( -63.73643367056612874, -223.0630224519699709, 88.93956664432811010 ) ) ;
#6650=CARTESIAN_POINT ( 'NONE',  ( -26.50000000000003197, 0.000000000000000000, 15.99999999999998579 ) ) ;
#6652=CARTESIAN_POINT ( 'NONE',  ( -61.29878583597043473, -218.0630238806674868, 91.75193312006507540 ) ) ;
#6653=ORIENTED_EDGE ( 'NONE', *, *, #1553, .T. ) ;
#6657=CARTESIAN_POINT ( 'NONE',  ( -24.15685424949240456, -108.3431457505074036, 36.34314575050753859 ) ) ;
#6668=( BOUNDED_CURVE ( )  B_SPLINE_CURVE ( 3, ( #4373, #7323, #1287, #6017 ),
 .UNSPECIFIED., .F., .T. ) 
 B_SPLINE_CURVE_WITH_KNOTS ( ( 4, 4 ),
 ( 3.839724354387529903, 4.329963465791605515 ),
 .UNSPECIFIED. ) 
 CURVE ( )  GEOMETRIC_REPRESENTATION_ITEM ( )  RATIONAL_B_SPLINE_CURVE ( ( 1.000000000000000000, 0.9800722126984331428, 0.9800722126984331428, 1.000000000000000000 ) ) 
 REPRESENTATION_ITEM ( '' )  );
#6679=CARTESIAN_POINT ( 'NONE',  ( -63.18650605524960184, -223.0633041053692409, 79.40656603074529585 ) ) ;
#6682=CIRCLE ( 'NONE', #777, 6.000000000000000000 ) ;
#6689=FACE_OUTER_BOUND ( 'NONE', #78, .T. ) ;
#6692=CARTESIAN_POINT ( 'NONE',  ( -26.50000000000002487, 16.00000000000007105, 30.68629150101529035 ) ) ;
#6699=ORIENTED_EDGE ( 'NONE', *, *, #2199, .F. ) ;
#6700=EDGE_CURVE ( 'NONE', #4517, #5471, #5485, .T. ) ;
#6703=( BOUNDED_CURVE ( )  B_SPLINE_CURVE ( 3, ( #6281, #4596, #7014, #2323 ),
 .UNSPECIFIED., .F., .T. ) 
 B_SPLINE_CURVE_WITH_KNOTS ( ( 4, 4 ),
 ( -1.776356839400250465E-15, 1.570796326794894782 ),
 .UNSPECIFIED. ) 
 CURVE ( )  GEOMETRIC_REPRESENTATION_ITEM ( )  RATIONAL_B_SPLINE_CURVE ( ( 1.000000000000000000, 0.8047378541243649375, 0.8047378541243649375, 1.000000000000000000 ) ) 
 REPRESENTATION_ITEM ( '' )  );
#6706=CARTESIAN_POINT ( 'NONE',  ( -64.50000000000000000, -49.37258300203047412, 0.000000000000000000 ) ) ;
#6711=CARTESIAN_POINT ( 'NONE',  ( -27.07790214619733860, -113.7796841263389069, 41.77968412633906325 ) ) ;
#6717=CARTESIAN_POINT ( 'NONE',  ( -30.49999999999998579, -218.0630240738404950, 95.20959099461346398 ) ) ;
#6720=CARTESIAN_POINT ( 'NONE',  ( -63.59161903724382370, -223.0630248190201144, 80.27589206438142355 ) ) ;
#6727=CARTESIAN_POINT ( 'NONE',  ( -53.17910001414514198, -221.3248423084432943, 72.81553374298380277 ) ) ;
#6728=CIRCLE ( 'NONE', #101, 15.99999999999999645 ) ;
#6729=PLANE ( 'NONE',  #545 ) ;
#6732=ORIENTED_EDGE ( 'NONE', *, *, #6624, .T. ) ;
#6738=ORIENTED_EDGE ( 'NONE', *, *, #2314, .T. ) ;
#6743=EDGE_LOOP ( 'NONE', ( #3596, #382, #6153, #521 ) ) ;
#6752=CARTESIAN_POINT ( 'NONE',  ( -53.96146975291424752, -223.0630240738406940, 73.28127814332049184 ) ) ;
#6761=CARTESIAN_POINT ( 'NONE',  ( -21.64859110346408144, -111.8253808406378766, 39.82538084063804007 ) ) ;
#6779=DIRECTION ( 'NONE',  ( 1.000000000000000000, 2.465190328815661892E-32, -9.244463733058732095E-33 ) ) ;
#6780=ORIENTED_EDGE ( 'NONE', *, *, #3100, .F. ) ;
#6788=B_SPLINE_CURVE_WITH_KNOTS ( 'NONE', 3,
 ( #3546, #2423, #1146, #7117, #4815, #4235, #5389, #1303 ),
 .UNSPECIFIED., .F., .F.,
 ( 4, 2, 2, 4 ),
 ( 0.000000000000000000, 0.4819498650539918438, 0.9733208903963990188, 1.000000000000000000 ),
 .UNSPECIFIED. ) ;
#6792=DIRECTION ( 'NONE',  ( 0.000000000000000000, 0.000000000000000000, 1.000000000000000000 ) ) ;
#6798=DIRECTION ( 'NONE',  ( 0.000000000000000000, 1.301042606982607490E-15, -1.000000000000000000 ) ) ;
#6799=CARTESIAN_POINT ( 'NONE',  ( -26.49999999999998224, 15.99999999999998579, 96.09122589815608251 ) ) ;
#6801=EDGE_CURVE ( 'NONE', #1413, #1433, #3935, .T. ) ;
#6808=CARTESIAN_POINT ( 'NONE',  ( -64.50000000000000000, -218.0630240738404950, 71.94153218116483117 ) ) ;
#6810=CARTESIAN_POINT ( 'NONE',  ( -23.84314575050760965, -63.65685424949226956, 36.65685424949239035 ) ) ;
#6817=DIRECTION ( 'NONE',  ( 1.078147950931789757E-16, 0.000000000000000000, 1.000000000000000000 ) ) ;
#6819=ORIENTED_EDGE ( 'NONE', *, *, #181, .F. ) ;
#6821=CARTESIAN_POINT ( 'NONE',  ( -60.75121803101544060, -218.1074892565148389, 95.21743140602129074 ) ) ;
#6831=LINE ( 'NONE', #2827, #6067 ) ;
#6833=CARTESIAN_POINT ( 'NONE',  ( -21.50000000000000000, -99.90626354475344328, 72.90626354475362803 ) ) ;
#6834=CARTESIAN_POINT ( 'NONE',  ( -55.98581939899504789, -218.0639615485030731, 72.31444438799266550 ) ) ;
#6838=EDGE_CURVE ( 'NONE', #6889, #4080, #5930, .T. ) ;
#6847=CARTESIAN_POINT ( 'NONE',  ( -26.50000000000003197, -49.37258300203047412, 0.000000000000000000 ) ) ;
#6849=CARTESIAN_POINT ( 'NONE',  ( -32.50000000000002132, -104.2695387347598199, 32.26953873475996204 ) ) ;
#6855=DIRECTION ( 'NONE',  ( -2.465190328815661892E-32, -1.000000000000000000, -1.193489751472043281E-15 ) ) ;
#6860=CARTESIAN_POINT ( 'NONE',  ( -26.50000000000000711, -117.1391065123254407, 44.37576177830231217 ) ) ;
#6868=CARTESIAN_POINT ( 'NONE',  ( -61.48006764033648608, -223.0630142795953361, 92.57606059409799570 ) ) ;
#6871=CARTESIAN_POINT ( 'NONE',  ( -63.71456966626824681, -218.0632277174277931, 79.42893510942502644 ) ) ;
#6874=ORIENTED_EDGE ( 'NONE', *, *, #1442, .T. ) ;
#6875=CARTESIAN_POINT ( 'NONE',  ( -29.50000000000000000, -223.0630240738404950, 96.09122589815579829 ) ) ;
#6877=CARTESIAN_POINT ( 'NONE',  ( -26.50000000000002842, -59.83638031753264386, 32.83638031753274333 ) ) ;
#6880=VECTOR ( 'NONE', #2480, 1000.000000000000000 ) ;
#6883=VECTOR ( 'NONE', #6032, 1000.000000000000000 ) ;
#6889=VERTEX_POINT ( 'NONE', #5665 ) ;
#6899=ADVANCED_FACE ( 'NONE', ( #2662, #389, #4437 ), #1004, .F. ) ;
#6906=CARTESIAN_POINT ( 'NONE',  ( -61.41022502515119896, -223.0630231714714569, 92.65062556679446004 ) ) ;
#6909=CARTESIAN_POINT ( 'NONE',  ( -61.41499871938025024, -218.0631008031258489, 75.68632222678733967 ) ) ;
#6910=EDGE_CURVE ( 'NONE', #312, #1071, #2165, .T. ) ;
#6921=DIRECTION ( 'NONE',  ( 1.000000000000000000, 2.465190328815661892E-32, -9.244463733058732095E-33 ) ) ;
#6927=CARTESIAN_POINT ( 'NONE',  ( -27.51602904742827604, -67.18204818810112045, 40.18204818810124124 ) ) ;
#6938=CARTESIAN_POINT ( 'NONE',  ( -69.99135978879996856, -227.6251019015761869, 80.18334626974976231 ) ) ;
#6946=AXIS2_PLACEMENT_3D ( 'NONE', #4603, #6949, #6288 ) ;
#6949=DIRECTION ( 'NONE',  ( -1.000000000000000000, -1.725633230170963324E-31, 1.078147950931789387E-16 ) ) ;
#6950=CARTESIAN_POINT ( 'NONE',  ( -64.50000000000000000, 0.000000000000000000, 0.000000000000000000 ) ) ;
#6953=CARTESIAN_POINT ( 'NONE',  ( -58.71195746406514360, -218.0634440981631599, 73.48571986131535994 ) ) ;
#6963=ORIENTED_EDGE ( 'NONE', *, *, #2800, .T. ) ;
#6965=DIRECTION ( 'NONE',  ( 1.000000000000000000, 4.437342591868191405E-31, -3.379803290564627108E-16 ) ) ;
#6967=CARTESIAN_POINT ( 'NONE',  ( -26.50000000000003197, 8.628166150854813118E-31, 6.000000000000001776 ) ) ;
#6968=EDGE_CURVE ( 'NONE', #5372, #2966, #3751, .T. ) ;
#6969=ORIENTED_EDGE ( 'NONE', *, *, #143, .T. ) ;
#6979=CARTESIAN_POINT ( 'NONE',  ( -32.50000000000002132, -39.68629150101520509, 16.00000000000001421 ) ) ;
#6987=ADVANCED_FACE ( 'NONE', ( #1963 ), #3705, .F. ) ;
#7001=CARTESIAN_POINT ( 'NONE',  ( -64.50000000000000000, -120.9522879036833274, 45.92078884797940219 ) ) ;
#7005=EDGE_CURVE ( 'NONE', #3994, #5048, #4563, .T. ) ;
#7011=ORIENTED_EDGE ( 'NONE', *, *, #336, .T. ) ;
#7014=CARTESIAN_POINT ( 'NONE',  ( -26.49999999999998224, -216.4061698243480976, 94.91744288732648727 ) ) ;
#7015=CARTESIAN_POINT ( 'NONE',  ( -26.50000000000003197, -49.37258300203047412, 0.000000000000000000 ) ) ;
#7040=CARTESIAN_POINT ( 'NONE',  ( -21.49999999999999645, -69.31370849898463860, 42.31370849898474518 ) ) ;
#7043=EDGE_LOOP ( 'NONE', ( #810, #4393, #5387, #2815 ) ) ;
#7056=VECTOR ( 'NONE', #2528, 1000.000000000000114 ) ;
#7066=ORIENTED_EDGE ( 'NONE', *, *, #5828, .F. ) ;
#7077=ORIENTED_EDGE ( 'NONE', *, *, #4763, .T. ) ;
#7078=PRODUCT_DEFINITION_SHAPE ( 'NONE', 'NONE',  #3350 ) ;
#7082=CARTESIAN_POINT ( 'NONE',  ( -70.12218822116579986, -219.3688186872617507, 89.73635190582676557 ) ) ;
#7094=CARTESIAN_POINT ( 'NONE',  ( -32.50000000000002132, -39.68629150101521930, 16.00000000000001421 ) ) ;
#7117=CARTESIAN_POINT ( 'NONE',  ( -53.33013951010422460, -219.8343230396700392, 95.52191879319023826 ) ) ;
#7119=CARTESIAN_POINT ( 'NONE',  ( -53.25562355766779632, -223.0194114314941771, 73.26959217102397304 ) ) ;
#7120=CARTESIAN_POINT ( 'NONE',  ( -63.57333428775314843, -218.0629783339272194, 88.28346941490387678 ) ) ;
#7141=DIRECTION ( 'NONE',  ( 0.000000000000000000, 1.000000000000000000, 1.734723475976805517E-15 ) ) ;
#7150=CARTESIAN_POINT ( 'NONE',  ( -26.50000000000003197, -60.68629150101524772, -11.31370849898474873 ) ) ;
#7153=CARTESIAN_POINT ( 'NONE',  ( -70.12218822116579986, -221.8025471834170332, 78.75851208262513126 ) ) ;
#7156=CARTESIAN_POINT ( 'NONE',  ( -63.51202228486167911, -218.0629290329284515, 88.42502795811738281 ) ) ;
#7164=FACE_OUTER_BOUND ( 'NONE', #3693, .T. ) ;
#7166=AXIS2_PLACEMENT_3D ( 'NONE', #7015, #7549, #4212 ) ;
#7174=ORIENTED_EDGE ( 'NONE', *, *, #6968, .F. ) ;
#7180=CARTESIAN_POINT ( 'NONE',  ( -63.40503953359656464, -223.0631132561157131, 79.85303703543833365 ) ) ;
#7182=VECTOR ( 'NONE', #879, 1000.000000000000000 ) ;
#7184=AXIS2_PLACEMENT_3D ( 'NONE', #768, #4864, #6622 ) ;
#7192=CARTESIAN_POINT ( 'NONE',  ( -53.47314606205194565, -223.0630240738404950, 96.09122589815579829 ) ) ;
#7193=CARTESIAN_POINT ( 'NONE',  ( -53.10580595754475297, -219.7017882839730873, 72.38063772785491778 ) ) ;
#7195=CARTESIAN_POINT ( 'NONE',  ( -63.88876000171747904, -218.0630240738404950, 87.48027644629948441 ) ) ;
#7220=CARTESIAN_POINT ( 'NONE',  ( -63.83803158340868578, -223.0628179935395963, 88.66427253312173207 ) ) ;
#7221=CARTESIAN_POINT ( 'NONE',  ( -53.25759302228803449, -223.0630240738404950, 73.28127814332044920 ) ) ;
#7223=ORIENTED_EDGE ( 'NONE', *, *, #6450, .F. ) ;
#7225=CARTESIAN_POINT ( 'NONE',  ( -26.50000000000002487, 16.00000000000012079, -15.99999999999995914 ) ) ;
#7226=CARTESIAN_POINT ( 'NONE',  ( -21.51784377693468642, -113.7796841263389069, 41.77968412633906325 ) ) ;
#7244=LINE ( 'NONE', #5408, #7259 ) ;
#7246=DIRECTION ( 'NONE',  ( 2.465190328815661892E-32, 0.7071067811865465735, -0.7071067811865484609 ) ) ;
#7252=SHAPE_REPRESENTATION ( 'right arm', ( #1914 ), #6207 ) ;
#7256=CARTESIAN_POINT ( 'NONE',  ( -63.27605943754021922, -223.0632182441923703, 79.58247367488434065 ) ) ;
#7259=VECTOR ( 'NONE', #745, 1000.000000000000000 ) ;
#7260=ORIENTED_EDGE ( 'NONE', *, *, #363, .T. ) ;
#7268=LINE ( 'NONE', #6692, #799 ) ;
#7274=VERTEX_POINT ( 'NONE', #1833 ) ;
#7277=ORIENTED_EDGE ( 'NONE', *, *, #4663, .T. ) ;
#7280=CARTESIAN_POINT ( 'NONE',  ( -64.50000000000000000, -223.0630240738404950, 73.28127814332044920 ) ) ;
#7283=( NAMED_UNIT ( * ) SI_UNIT ( $, .STERADIAN. ) SOLID_ANGLE_UNIT ( ) );
#7291=DIRECTION ( 'NONE',  ( 1.000000000000000000, 2.465190328815661892E-32, -9.244463733058732095E-33 ) ) ;
#7292=CARTESIAN_POINT ( 'NONE',  ( -64.48438679943396323, -223.0632018673171331, 84.15020320440139301 ) ) ;
#7304=VECTOR ( 'NONE', #6779, 1000.000000000000000 ) ;
#7305=PLANE ( 'NONE',  #1007 ) ;
#7315=PRODUCT_DEFINITION_FORMATION_WITH_SPECIFIED_SOURCE ( 'ANY', '', #5293, .NOT_KNOWN. ) ;
#7323=CARTESIAN_POINT ( 'NONE',  ( -28.34608510185598718, -111.4855484589742645, 39.48554845897440657 ) ) ;
#7326=VECTOR ( 'NONE', #3343, 1000.000000000000000 ) ;
#7333=CARTESIAN_POINT ( 'NONE',  ( -53.25759302228803449, -223.0630240738404950, 73.28127814332044920 ) ) ;
#7339=VERTEX_POINT ( 'NONE', #255 ) ;
#7340=ORIENTED_EDGE ( 'NONE', *, *, #4594, .F. ) ;
#7345=LINE ( 'NONE', #4972, #5838 ) ;
#7352=CARTESIAN_POINT ( 'NONE',  ( -30.49999999999999289, -218.0630240738404950, 71.94153218116483117 ) ) ;
#7355=CARTESIAN_POINT ( 'NONE',  ( -60.81252276423128933, -222.2597742987536833, 95.94959129056178426 ) ) ;
#7357=CARTESIAN_POINT ( 'NONE',  ( -29.64230087749236731, -65.39789427971169289, 38.39789427971179947 ) ) ;
#7366=CARTESIAN_POINT ( 'NONE',  ( -58.41284488070792946, -223.0628661248926221, 94.90319541541143167 ) ) ;
#7370=VECTOR ( 'NONE', #4450, 1000.000000000000114 ) ;
#7371=VERTEX_POINT ( 'NONE', #6169 ) ;
#7372=VERTEX_POINT ( 'NONE', #184 ) ;
#7379=EDGE_LOOP ( 'NONE', ( #6653, #4699, #5790, #6391, #5360, #4130, #4959, #6070 ) ) ;
#7381=EDGE_CURVE ( 'NONE', #4282, #1164, #3688, .T. ) ;
#7387=DIRECTION ( 'NONE',  ( 0.000000000000000000, 1.301042606982602363E-15, -1.000000000000000000 ) ) ;
#7392=CARTESIAN_POINT ( 'NONE',  ( -60.82928583850154070, -223.3951688904013793, 96.14979199081719230 ) ) ;
#7394=CARTESIAN_POINT ( 'NONE',  ( -24.15685424949240456, -108.3431457505074036, 36.34314575050753859 ) ) ;
#7398=CARTESIAN_POINT ( 'NONE',  ( -32.50000000000002132, 0.000000000000000000, 15.99999999999998579 ) ) ;
#7400=CARTESIAN_POINT ( 'NONE',  ( -61.39623761241656297, -223.0630238903453062, 92.66543157068049652 ) ) ;
#7403=CARTESIAN_POINT ( 'NONE',  ( -63.98735188657113326, -218.0643623503109723, 80.21364601424980378 ) ) ;
#7430=ORIENTED_EDGE ( 'NONE', *, *, #6176, .F. ) ;
#7433=DIRECTION ( 'NONE',  ( -3.379803290564627601E-16, 1.193489751472043281E-15, -1.000000000000000000 ) ) ;
#7438=CARTESIAN_POINT ( 'NONE',  ( -53.43756829269602804, -222.2597742987530012, 95.94959129055985159 ) ) ;
#7441=ORIENTED_EDGE ( 'NONE', *, *, #3842, .T. ) ;
#7446=DIRECTION ( 'NONE',  ( 0.000000000000000000, 0.000000000000000000, 1.000000000000000000 ) ) ;
#7448=CARTESIAN_POINT ( 'NONE',  ( -61.58697569811064199, -218.0631950677025372, 75.87810468754312865 ) ) ;
#7470=CARTESIAN_POINT ( 'NONE',  ( -21.50000000000000000, -215.0630240738404950, 71.13768460387149162 ) ) ;
#7472=LINE ( 'NONE', #3323, #1991 ) ;
#7480=CARTESIAN_POINT ( 'NONE',  ( -62.46707313028079511, -223.0624047416972928, 91.35632827828391100 ) ) ;
#7484=CARTESIAN_POINT ( 'NONE',  ( -63.59542962824011880, -218.0630242179433083, 79.12967373414080896 ) ) ;
#7489=CARTESIAN_POINT ( 'NONE',  ( -25.67719663180531597, -61.82280336819460587, 34.82280336819470534 ) ) ;
#7493=EDGE_CURVE ( 'NONE', #7371, #4795, #919, .T. ) ;
#7496=( BOUNDED_CURVE ( )  B_SPLINE_CURVE ( 3, ( #7357, #5753, #1502, #4524 ),
 .UNSPECIFIED., .F., .T. ) 
 B_SPLINE_CURVE_WITH_KNOTS ( ( 4, 4 ),
 ( 0.6981317007977413391, 1.570796326794899223 ),
 .UNSPECIFIED. ) 
 CURVE ( )  GEOMETRIC_REPRESENTATION_ITEM ( )  RATIONAL_B_SPLINE_CURVE ( ( 1.000000000000000000, 0.9375385246911008830, 0.9375385246911008830, 1.000000000000000000 ) ) 
 REPRESENTATION_ITEM ( '' )  );
#7501=AXIS2_PLACEMENT_3D ( 'NONE', #2616, #2579, #3783 ) ;
#7505=CYLINDRICAL_SURFACE ( 'NONE', #2381, 7.999999999999986677 ) ;
#7508=CARTESIAN_POINT ( 'NONE',  ( -53.40199052334512686, -221.4565245236570945, 95.80795668296245537 ) ) ;
#7513=VERTEX_POINT ( 'NONE', #5637 ) ;
#7517=CARTESIAN_POINT ( 'NONE',  ( -63.72819125881465396, -223.0630240445839547, 88.96101468828511827 ) ) ;
#7518=DIRECTION ( 'NONE',  ( 1.000000000000000000, 2.465190328815661892E-32, -9.244463733058732095E-33 ) ) ;
#7520=CARTESIAN_POINT ( 'NONE',  ( -64.08462656067526098, -218.0647558284272804, 80.54457062688838676 ) ) ;
#7531=CARTESIAN_POINT ( 'NONE',  ( -28.15685424949236548, -218.0630240738404666, 71.94153218116485959 ) ) ;
#7540=VERTEX_POINT ( 'NONE', #5141 ) ;
#7541=DIRECTION ( 'NONE',  ( 0.000000000000000000, 0.000000000000000000, 1.000000000000000000 ) ) ;
#7549=DIRECTION ( 'NONE',  ( 1.000000000000000000, 2.465190328815661892E-32, -9.244463733058732095E-33 ) ) ;
#7560=CARTESIAN_POINT ( 'NONE',  ( -58.23354184286210966, -218.0632466406002834, 73.22543673403131947 ) ) ;
#7561=VERTEX_POINT ( 'NONE', #4144 ) ;
#7565=PLANE ( 'NONE',  #5592 ) ;
#7572=CARTESIAN_POINT ( 'NONE',  ( -26.50000000000003197, -45.34314575050759544, 18.34314575050763452 ) ) ;
#7574=CARTESIAN_POINT ( 'NONE',  ( -32.50000000000002842, -7.347880794884118750E-16, -6.000000000000001776 ) ) ;
#7579=ORIENTED_EDGE ( 'NONE', *, *, #1176, .F. ) ;
#7580=VECTOR ( 'NONE', #1971, 1000.000000000000000 ) ;
#7582=CYLINDRICAL_SURFACE ( 'NONE', #3247, 15.99999999999998934 ) ;
#7587=CARTESIAN_POINT ( 'NONE',  ( -26.50000000000003197, -57.68629150101511271, 30.68629150101523351 ) ) ;
#7597=FACE_OUTER_BOUND ( 'NONE', #973, .T. ) ;
#7625=COLOUR_RGB('Sky Blue',0.24,0.69,0.87);
#7626=FILL_AREA_STYLE_COLOUR('',#7625);
#7627=FILL_AREA_STYLE('',(#7626));
#7628=SURFACE_STYLE_FILL_AREA(#7627);
#7629=SURFACE_SIDE_STYLE('',(#7628));
#7630=SURFACE_STYLE_USAGE(.BOTH.,#7629);
#7631=PRESENTATION_STYLE_ASSIGNMENT((#7630));
ENDSEC;
END-ISO-10303-21;
